ISO-10303-21;
HEADER;
FILE_DESCRIPTION (('STEP AP214'),
    '1' );
FILE_NAME ('hex flange bolt small_iso_ISO 4162 - M8 x 45 x 22-N.step',
    '2026-10-25T07:12:54',
    ( '' ),
    ( '' ),
    'SwSTEP 2.0',
    'SolidWorks 2026',
    '' );
FILE_SCHEMA (( 'AUTOMOTIVE_DESIGN' ));
ENDSEC;

DATA;
#29=ORIENTED_EDGE ( 'NONE', *, *, #7296, .F. ) ;
#33=AXIS2_PLACEMENT_3D ( 'NONE', #4037, #13487, #9223 ) ;
#43=CARTESIAN_POINT ( 'NONE',  ( 6.367873360227555679, -2.886751345948119774, 4.999999999999999112 ) ) ;
#48=TOROIDAL_SURFACE ( 'NONE', #12842, 7.900000000000002132, 0.5999999999999979794 ) ;
#52=EDGE_CURVE ( 'NONE', #12021, #8324, #11821, .T. ) ;
#63=( LENGTH_UNIT ( ) NAMED_UNIT ( * ) SI_UNIT ( .MILLI., .METRE. ) );
#69=CARTESIAN_POINT ( 'NONE',  ( 6.207671477327291853, -3.321994320370684317, 4.246137054662720622 ) ) ;
#83=CIRCLE ( 'NONE', #7166, 4.999999999999999112 ) ;
#90=CARTESIAN_POINT ( 'NONE',  ( 0.08165819712376973238, 4.939961795957293234, 1.443735181952769064 ) ) ;
#112=CARTESIAN_POINT ( 'NONE',  ( 6.466260427357665819, -5.808561367196025671, 1.503437176544561004E-15 ) ) ;
#147=CONICAL_SURFACE ( 'NONE', #11179, 8.105212085995399107, 1.221730476396037490 ) ;
#175=CARTESIAN_POINT ( 'NONE',  ( 6.527192678185836705, -5.883244248022288403, -1.193258867985458992E-13 ) ) ;
#195=B_SPLINE_CURVE_WITH_KNOTS ( 'NONE', 3,
 ( #11262, #10080, #4985, #5816, #13250 ),
 .UNSPECIFIED., .F., .F.,
 ( 4, 1, 4 ),
 ( 0.000000000000000000, 0.002886751345948130286, 0.005773502691896260572 ),
 .UNSPECIFIED. ) ;
#235=CARTESIAN_POINT ( 'NONE',  ( 6.527192678185834041, 2.941622124011172623, 5.095038975455953079 ) ) ;
#268=DIRECTION ( 'NONE',  ( 0.3420201433256622736, 0.000000000000000000, -0.9396926207859106484 ) ) ;
#285=CARTESIAN_POINT ( 'NONE',  ( 0.4465819873852002742, 2.886751345948125547, 4.999999999999999112 ) ) ;
#291=DIRECTION ( 'NONE',  ( 0.000000000000000000, -1.000000000000000000, 0.000000000000000000 ) ) ;
#303=AXIS2_PLACEMENT_3D ( 'NONE', #3624, #7847, #12122 ) ;
#325=EDGE_CURVE ( 'NONE', #12408, #8324, #8870, .T. ) ;
#332=ORIENTED_EDGE ( 'NONE', *, *, #7882, .F. ) ;
#371=CARTESIAN_POINT ( 'NONE',  ( 6.367873360227556567, 2.886751345948123770, -5.000000000000000000 ) ) ;
#382=DIRECTION ( 'NONE',  ( 0.000000000000000000, 0.000000000000000000, 1.000000000000000000 ) ) ;
#394=AXIS2_PLACEMENT_3D ( 'NONE', #8294, #11541, #12425 ) ;
#395=ADVANCED_FACE ( 'NONE', ( #9439 ), #5005, .T. ) ;
#430=AXIS2_PLACEMENT_3D ( 'NONE', #5828, #10990, #3471 ) ;
#446=ADVANCED_FACE ( 'NONE', ( #3219 ), #7312, .F. ) ;
#459=ORIENTED_EDGE ( 'NONE', *, *, #1514, .T. ) ;
#473=ORIENTED_EDGE ( 'NONE', *, *, #13349, .F. ) ;
#484=DIRECTION ( 'NONE',  ( -1.000000000000000000, -0.000000000000000000, -0.000000000000000000 ) ) ;
#486=VERTEX_POINT ( 'NONE', #3975 ) ;
#507=ORIENTED_EDGE ( 'NONE', *, *, #8494, .T. ) ;
#532=CARTESIAN_POINT ( 'NONE',  ( 5.991014884144048480, -4.770489558936219510E-15, -5.000000000000000000 ) ) ;
#595=ORIENTED_EDGE ( 'NONE', *, *, #9564, .F. ) ;
#599=CARTESIAN_POINT ( 'NONE',  ( 0.000000000000000000, 4.330127018922190985, 2.500000000000005329 ) ) ;
#602=DIRECTION ( 'NONE',  ( 0.000000000000000000, 0.000000000000000000, 1.000000000000000000 ) ) ;
#618=CARTESIAN_POINT ( 'NONE',  ( 0.4465819873852039379, 5.773502691896261751, 3.331019006688249527E-17 ) ) ;
#637=CARTESIAN_POINT ( 'NONE',  ( 6.327632967271008546, -3.313549392874691524, -4.260764098152702850 ) ) ;
#656=CARTESIAN_POINT ( 'NONE',  ( 6.481779955677435368, -2.910222513313295511, -5.040653254389411586 ) ) ;
#670=ORIENTED_EDGE ( 'NONE', *, *, #2051, .T. ) ;
#682=FACE_OUTER_BOUND ( 'NONE', #4570, .T. ) ;
#693=CARTESIAN_POINT ( 'NONE',  ( 0.000000000000000000, -4.330127018922193649, -2.500000000000000000 ) ) ;
#712=CARTESIAN_POINT ( 'NONE',  ( 6.534533895392292457, -2.951347675328713116, 5.111884124469662893 ) ) ;
#748=CARTESIAN_POINT ( 'NONE',  ( 6.534838248920899595, 5.903531555104835071, 8.098083288904839678E-18 ) ) ;
#766=PRODUCT_CONTEXT ( 'NONE', #12286, 'mechanical' ) ;
#773=CARTESIAN_POINT ( 'NONE',  ( 6.534838248920897819, 2.951765777552412651, 5.112608298763836601 ) ) ;
#783=AXIS2_PLACEMENT_3D ( 'NONE', #1118, #7239, #5238 ) ;
#785=CARTESIAN_POINT ( 'NONE',  ( 6.506987859255527695, -2.925375531177290878, 5.066899051217877314 ) ) ;
#798=ORIENTED_EDGE ( 'NONE', *, *, #2783, .T. ) ;
#801=CARTESIAN_POINT ( 'NONE',  ( 8.500000000000000000, 2.886751345948123770, -5.000000000000000000 ) ) ;
#826=CARTESIAN_POINT ( 'NONE',  ( 0.1739375980333736638, 5.301268757141562205, -0.8179331680533008520 ) ) ;
#844=VERTEX_POINT ( 'NONE', #13077 ) ;
#852=FACE_OUTER_BOUND ( 'NONE', #11629, .T. ) ;
#853=PRESENTATION_STYLE_ASSIGNMENT (( #8281 ) ) ;
#870=ADVANCED_BREP_SHAPE_REPRESENTATION ( '', ( #5623, #430 ), #7942 ) ;
#901=CARTESIAN_POINT ( 'NONE',  ( 6.420058897733097680, 2.891482565094591006, -5.008194711943424693 ) ) ;
#926=CARTESIAN_POINT ( 'NONE',  ( 6.362374563308273778, -3.415000007734520171, -4.302769906043296011 ) ) ;
#955=CARTESIAN_POINT ( 'NONE',  ( 6.534838248920897819, 2.951765777552411318, -5.112608298763837489 ) ) ;
#971=CARTESIAN_POINT ( 'NONE',  ( 6.385552186430389021, 5.773502691896261751, 0.000000000000000000 ) ) ;
#972=CARTESIAN_POINT ( 'NONE',  ( 6.452281807715818829, 2.898928808472990948, -5.021091983800339165 ) ) ;
#981=LINE ( 'NONE', #9300, #11977 ) ;
#988=ORIENTED_EDGE ( 'NONE', *, *, #1729, .F. ) ;
#992=CARTESIAN_POINT ( 'NONE',  ( 6.212075932873402984, -2.040040303548923628, 4.999999999999999112 ) ) ;
#1013=ADVANCED_FACE ( 'NONE', ( #3914 ), #6499, .T. ) ;
#1049=DIRECTION ( 'NONE',  ( -1.000000000000000000, -0.000000000000000000, -0.000000000000000000 ) ) ;
#1056=( GEOMETRIC_REPRESENTATION_CONTEXT ( 3 ) GLOBAL_UNCERTAINTY_ASSIGNED_CONTEXT ( ( #8827 ) ) GLOBAL_UNIT_ASSIGNED_CONTEXT ( ( #63, #2260, #8567 ) ) REPRESENTATION_CONTEXT ( 'NONE', 'WORKASPACE' ) );
#1079=AXIS2_PLACEMENT_3D ( 'NONE', #9191, #11258, #1779 ) ;
#1085=CARTESIAN_POINT ( 'NONE',  ( 6.534838248920899595, -2.951765777552420644, -5.112608298763837489 ) ) ;
#1112=CARTESIAN_POINT ( 'NONE',  ( 0.000000000000000000, 4.330127018922190985, 2.500000000000005329 ) ) ;
#1118=CARTESIAN_POINT ( 'NONE',  ( 8.500000000000000000, -5.773502691896263528, 0.000000000000000000 ) ) ;
#1119=ORIENTED_EDGE ( 'NONE', *, *, #325, .F. ) ;
#1141=ORIENTED_EDGE ( 'NONE', *, *, #6219, .T. ) ;
#1143=CARTESIAN_POINT ( 'NONE',  ( 6.534838248920897819, 2.951765777552411318, -5.112608298763837489 ) ) ;
#1160=B_SPLINE_CURVE_WITH_KNOTS ( 'NONE', 3,
 ( #4393, #3360, #9652, #6425, #175, #11791, #6614, #7584, #12749, #112, #7453, #3293, #1260, #9787, #8755, #7720 ),
 .UNSPECIFIED., .F., .F.,
 ( 4, 3, 3, 3, 3, 4 ),
 ( -2.669610558405663348E-06, 0.000000000000000000, 5.703179328867284594E-05, 0.0001157653700806020010, 0.0001686517580799737359, 0.0002219032271235107196 ),
 .UNSPECIFIED. ) ;
#1173=CARTESIAN_POINT ( 'NONE',  ( 6.466260427357672924, 2.904280683598007951, -5.030361703432632225 ) ) ;
#1244=CARTESIAN_POINT ( 'NONE',  ( 0.3106000600989293203, 5.537975084925940372, 0.4079457818577097994 ) ) ;
#1260=CARTESIAN_POINT ( 'NONE',  ( 6.420058897733094128, -5.782965130189196223, 5.134498127650324400E-16 ) ) ;
#1263=ADVANCED_FACE ( 'NONE', ( #7900 ), #147, .T. ) ;
#1265=EDGE_CURVE ( 'NONE', #3640, #5736, #4961, .T. ) ;
#1281=AXIS2_PLACEMENT_3D ( 'NONE', #8689, #11723, #10814 ) ;
#1296=AXIS2_PLACEMENT_3D ( 'NONE', #6982, #3932, #10153 ) ;
#1298=DIRECTION ( 'NONE',  ( 0.000000000000000000, 0.5000000000000009992, -0.8660254037844380415 ) ) ;
#1305=ORIENTED_EDGE ( 'NONE', *, *, #10213, .F. ) ;
#1321=DIRECTION ( 'NONE',  ( 0.000000000000000000, 0.000000000000000000, -1.000000000000000000 ) ) ;
#1326=CYLINDRICAL_SURFACE ( 'NONE', #6419, 4.000000000000000000 ) ;
#1339=CARTESIAN_POINT ( 'NONE',  ( 0.08165819712376803929, -3.720292241887084295, 3.556264818047238041 ) ) ;
#1346=AXIS2_PLACEMENT_3D ( 'NONE', #5985, #5016, #6127 ) ;
#1351=AXIS2_PLACEMENT_3D ( 'NONE', #7867, #10130, #382 ) ;
#1355=EDGE_LOOP ( 'NONE', ( #6215, #4217, #7502, #11183 ) ) ;
#1371=ORIENTED_EDGE ( 'NONE', *, *, #6219, .F. ) ;
#1387=CARTESIAN_POINT ( 'NONE',  ( -6.315157543962389260E-16, -3.838309248099061044, -3.351853367130940065 ) ) ;
#1399=CARTESIAN_POINT ( 'NONE',  ( 0.000000000000000000, -4.330127018922193649, -2.500000000000000000 ) ) ;
#1401=CIRCLE ( 'NONE', #8276, 8.105212085995399107 ) ;
#1412=CARTESIAN_POINT ( 'NONE',  ( 6.323279575526388641, 5.335162385629701909, 0.7592276814629709270 ) ) ;
#1477=( NAMED_UNIT ( * ) SI_UNIT ( $, .STERADIAN. ) SOLID_ANGLE_UNIT ( ) );
#1487=ORIENTED_EDGE ( 'NONE', *, *, #7648, .T. ) ;
#1509=CARTESIAN_POINT ( 'NONE',  ( 6.534838248920897819, 2.951765777552411318, -5.112608298763837489 ) ) ;
#1511=EDGE_CURVE ( 'NONE', #7656, #12408, #1806, .T. ) ;
#1514=EDGE_CURVE ( 'NONE', #13345, #4029, #4299, .T. ) ;
#1540=FACE_OUTER_BOUND ( 'NONE', #3449, .T. ) ;
#1547=LINE ( 'NONE', #3645, #6476 ) ;
#1551=CARTESIAN_POINT ( 'NONE',  ( 6.507056081706568129, -2.993351035583803110, -4.999999999999999112 ) ) ;
#1565=CARTESIAN_POINT ( 'NONE',  ( 5.991014884144049368, -4.330127018922197202, -2.500000000000000444 ) ) ;
#1572=CIRCLE ( 'NONE', #5145, 4.000000000000000000 ) ;
#1589=DIRECTION ( 'NONE',  ( 0.000000000000000000, 0.000000000000000000, -1.000000000000000000 ) ) ;
#1594=B_SPLINE_CURVE_WITH_KNOTS ( 'NONE', 3,
 ( #2150, #8591, #8332, #6270, #6334, #8395 ),
 .UNSPECIFIED., .F., .F.,
 ( 4, 2, 4 ),
 ( 0.01506847346324404271, 0.01653041426658209689, 0.01799235506992015107 ),
 .UNSPECIFIED. ) ;
#1598=CARTESIAN_POINT ( 'NONE',  ( 6.207682235857189035, 2.016324304256315258, 4.999999999999999112 ) ) ;
#1612=CARTESIAN_POINT ( 'NONE',  ( 8.500000000000000000, 0.000000000000000000, 0.000000000000000000 ) ) ;
#1663=ORIENTED_EDGE ( 'NONE', *, *, #10213, .T. ) ;
#1664=( BOUNDED_SURFACE ( )  B_SPLINE_SURFACE ( 3, 2, ( 
 ( #13580, #3086, #7317 ),
 ( #992, #5244, #9444 ),
 ( #2105, #6352, #11848 ),
 ( #13081, #10945, #5641 ),
 ( #1598, #9713, #8811 ),
 ( #5707, #8682, #10807 ) ),
 .UNSPECIFIED., .F., .F., .T. ) 
 B_SPLINE_SURFACE_WITH_KNOTS ( ( 4, 2, 4 ),
 ( 3, 3 ),
 ( 0.02367497856332483747, 0.02662799652435013376, 0.02958101448537543005 ),
 ( 0.000000000000000000, 1.000000000000000000 ),
 .UNSPECIFIED. ) 
 GEOMETRIC_REPRESENTATION_ITEM ( )  RATIONAL_B_SPLINE_SURFACE ( (
 ( 1.000000000000000000, 0.8047781226141854649, 1.000000000000000000),
 ( 1.000000000000000000, 0.8123782257049820821, 1.000000000000000000),
 ( 1.000000000000000000, 0.8190665358012705344, 1.000000000000000000),
 ( 1.000000000000000000, 0.8192358187342196896, 1.000000000000000000),
 ( 1.000000000000000000, 0.8126132506074239537, 1.000000000000000000),
 ( 1.000000000000000000, 0.8047712440299316095, 1.000000000000000000) ) ) 
 REPRESENTATION_ITEM ( '' )  SURFACE ( )  );
#1666=ORIENTED_EDGE ( 'NONE', *, *, #12441, .F. ) ;
#1685=CARTESIAN_POINT ( 'NONE',  ( 6.245824673232814206, -3.903127342723638371, -3.450227696316022996 ) ) ;
#1687=CARTESIAN_POINT ( 'NONE',  ( 6.092449800118089343, 4.833012432206481357, 1.628976913806340798 ) ) ;
#1699=ORIENTED_EDGE ( 'NONE', *, *, #4647, .T. ) ;
#1700=ORIENTED_EDGE ( 'NONE', *, *, #6637, .T. ) ;
#1729=EDGE_CURVE ( 'NONE', #11948, #11251, #12889, .T. ) ;
#1731=CARTESIAN_POINT ( 'NONE',  ( 0.000000000000000000, 0.000000000000000000, 0.000000000000000000 ) ) ;
#1735=VERTEX_POINT ( 'NONE', #7119 ) ;
#1763=CARTESIAN_POINT ( 'NONE',  ( 6.541171952014627422, 2.986180817377861896, -5.112746308113085725 ) ) ;
#1772=ORIENTED_EDGE ( 'NONE', *, *, #9738, .F. ) ;
#1779=DIRECTION ( 'NONE',  ( 0.000000000000000000, 0.000000000000000000, -1.000000000000000000 ) ) ;
#1782=FACE_OUTER_BOUND ( 'NONE', #10657, .T. ) ;
#1789=ORIENTED_EDGE ( 'NONE', *, *, #8633, .F. ) ;
#1796=CARTESIAN_POINT ( 'NONE',  ( 0.4465819873851989974, -2.886751345948120218, 4.999999999999999112 ) ) ;
#1806=B_SPLINE_CURVE_WITH_KNOTS ( 'NONE', 3,
 ( #4155, #10447, #9415, #955 ),
 .UNSPECIFIED., .F., .F.,
 ( 4, 4 ),
 ( 0.002977824986803859555, 0.005972417098209359745 ),
 .UNSPECIFIED. ) ;
#1811=ORIENTED_EDGE ( 'NONE', *, *, #7648, .F. ) ;
#1820=CARTESIAN_POINT ( 'NONE',  ( 52.80949999999998568, 0.000000000000000000, 0.000000000000000000 ) ) ;
#1823=CARTESIAN_POINT ( 'NONE',  ( 0.000000000000000000, 0.000000000000000000, -5.000000000000000000 ) ) ;
#1829=CARTESIAN_POINT ( 'NONE',  ( 6.390983399715591595, 2.822795037344616897, -5.110775575965828210 ) ) ;
#1834=CARTESIAN_POINT ( 'NONE',  ( 6.095462721915160920, 1.047438013718291705, -5.000000000000000000 ) ) ;
#1849=CARTESIAN_POINT ( 'NONE',  ( 6.196878017913832970, -3.367876570272822168, -4.166666666666666963 ) ) ;
#1851=CARTESIAN_POINT ( 'NONE',  ( 7.336184427528458230, 0.000000000000000000, -8.105212085995399107 ) ) ;
#1859=ORIENTED_EDGE ( 'NONE', *, *, #52, .F. ) ;
#1884=CARTESIAN_POINT ( 'NONE',  ( 0.000000000000000000, 4.330127018922190096, -2.500000000000006217 ) ) ;
#1894=CARTESIAN_POINT ( 'NONE',  ( 8.500000000000000000, 5.773502691896261751, -2.749426538070115714E-16 ) ) ;
#1904=SURFACE_SIDE_STYLE ('',( #11450 ) ) ;
#1947=CARTESIAN_POINT ( 'NONE',  ( 6.533910050139697390, 5.901028503456123175, 1.520834953648585461E-14 ) ) ;
#1948=CARTESIAN_POINT ( 'NONE',  ( 6.534838248920897819, 2.951765777552411318, -5.112608298763837489 ) ) ;
#1953=SHAPE_DEFINITION_REPRESENTATION ( #5881, #9196 ) ;
#1970=ORIENTED_EDGE ( 'NONE', *, *, #5773, .F. ) ;
#1997=CARTESIAN_POINT ( 'NONE',  ( 6.367873360227559232, -5.773502691896263528, 0.000000000000000000 ) ) ;
#1998=VECTOR ( 'NONE', #268, 1000.000000000000114 ) ;
#2001=ORIENTED_EDGE ( 'NONE', *, *, #13529, .F. ) ;
#2003=ORIENTED_EDGE ( 'NONE', *, *, #11505, .F. ) ;
#2007=CARTESIAN_POINT ( 'NONE',  ( 6.095473853218515536, -4.853892138987517590, 1.592812200814445633 ) ) ;
#2035=ORIENTED_EDGE ( 'NONE', *, *, #8494, .F. ) ;
#2037=EDGE_LOOP ( 'NONE', ( #1141, #13502, #3151, #1789, #6299, #5735, #9395 ) ) ;
#2044=CARTESIAN_POINT ( 'NONE',  ( 0.4465819873852039379, 5.773502691896261751, 3.331019006688249527E-17 ) ) ;
#2046=CARTESIAN_POINT ( 'NONE',  ( 5.991014884144047592, -4.330127018922191873, 2.499999999999998668 ) ) ;
#2051=EDGE_CURVE ( 'NONE', #11355, #9438, #7121, .T. ) ;
#2061=B_SPLINE_CURVE_WITH_KNOTS ( 'NONE', 3,
 ( #7643, #2237, #2168, #11847 ),
 .UNSPECIFIED., .F., .F.,
 ( 4, 4 ),
 ( 2.380735200831979558E-07, 0.002921158011986727237 ),
 .UNSPECIFIED. ) ;
#2071=CARTESIAN_POINT ( 'NONE',  ( 6.244889965166096069, -3.924082311521025712, -3.413878157001049907 ) ) ;
#2083=ORIENTED_EDGE ( 'NONE', *, *, #11849, .F. ) ;
#2099=B_SPLINE_CURVE_WITH_KNOTS ( 'NONE', 3,
 ( #2612, #1849, #1565, #11115, #11326 ),
 .UNSPECIFIED., .F., .F.,
 ( 4, 1, 4 ),
 ( 0.000000000000000000, 0.002886751345948128985, 0.005773502691896257970 ),
 .UNSPECIFIED. ) ;
#2101=CARTESIAN_POINT ( 'NONE',  ( 53.50000000000000000, 0.000000000000000000, 0.000000000000000000 ) ) ;
#2105=CARTESIAN_POINT ( 'NONE',  ( 6.095484975317565279, -1.047622383848427985, 4.999999999999999112 ) ) ;
#2136=CARTESIAN_POINT ( 'NONE',  ( 6.212068001624178493, -5.350125758160219291, 0.7333103599835463227 ) ) ;
#2148=CARTESIAN_POINT ( 'NONE',  ( 6.533910050139693837, 2.950514251728067361, -5.110440592449059238 ) ) ;
#2150=CARTESIAN_POINT ( 'NONE',  ( 0.4465819873852006072, 2.886751345948123770, -5.000000000000000000 ) ) ;
#2157=AXIS2_PLACEMENT_3D ( 'NONE', #5156, #6268, #4235 ) ;
#2167=CONICAL_SURFACE ( 'NONE', #394, 5.000000000000000000, 1.047197551196600296 ) ;
#2168=CARTESIAN_POINT ( 'NONE',  ( -3.917148844556152511E-15, -4.821944789745365334, 1.648146632869001094 ) ) ;
#2201=CARTESIAN_POINT ( 'NONE',  ( 6.357976367241810145, -3.426708043488799760, 4.282301071214263288 ) ) ;
#2237=CARTESIAN_POINT ( 'NONE',  ( 0.1739375980333740523, -5.301268757141563093, 0.8179331680533010740 ) ) ;
#2251=CARTESIAN_POINT ( 'NONE',  ( 0.1983443223721553794, -3.359771601077102154, 4.180704885107414448 ) ) ;
#2260=( NAMED_UNIT ( * ) PLANE_ANGLE_UNIT ( ) SI_UNIT ( $, .RADIAN. ) );
#2263=EDGE_LOOP ( 'NONE', ( #13482, #7170, #7393, #11395, #11422 ) ) ;
#2289=B_SPLINE_CURVE_WITH_KNOTS ( 'NONE', 3,
 ( #7864, #4816, #8280, #7245, #13299, #13506, #6147, #6002, #9312, #785, #10411, #9176, #6221, #10128, #712, #5033 ),
 .UNSPECIFIED., .F., .F.,
 ( 4, 3, 3, 3, 3, 4 ),
 ( 0.000000000000000000, 5.303647860849932744E-05, 0.0001057093501027352823, 0.0001642058037231763413, 0.0002210073443958810151, 0.0002236769549542870245 ),
 .UNSPECIFIED. ) ;
#2295=DIRECTION ( 'NONE',  ( 0.000000000000000000, 0.000000000000000000, -1.000000000000000000 ) ) ;
#2310=DIRECTION ( 'NONE',  ( -1.000000000000000000, -0.000000000000000000, -0.000000000000000000 ) ) ;
#2351=LINE ( 'NONE', #5619, #6380 ) ;
#2359=CARTESIAN_POINT ( 'NONE',  ( 0.1983443223721582938, 5.300482436767278038, 0.8192951148925896598 ) ) ;
#2367=CARTESIAN_POINT ( 'NONE',  ( 6.196878017913834746, 1.924500897298752955, 5.000000000000000000 ) ) ;
#2378=CARTESIAN_POINT ( 'NONE',  ( 0.000000000000000000, 0.000000000000000000, 5.000000000000000000 ) ) ;
#2383=AXIS2_PLACEMENT_3D ( 'NONE', #1612, #6755, #5721 ) ;
#2387=CARTESIAN_POINT ( 'NONE',  ( 0.4465819873852002742, 2.886751345948125547, 4.999999999999999112 ) ) ;
#2395=CIRCLE ( 'NONE', #9902, 8.105212085995399107 ) ;
#2397=B_SPLINE_CURVE_WITH_KNOTS ( 'NONE', 3,
 ( #3370, #7595, #4473, #6560, #1339, #2251, #6365, #9797 ),
 .UNSPECIFIED., .F., .F.,
 ( 4, 2, 2, 4 ),
 ( 0.002921158011986727237, 0.003648658599403079624, 0.004376159186819432445, 0.005831160361652135485 ),
 .UNSPECIFIED. ) ;
#2419=DIRECTION ( 'NONE',  ( -0.7071067811865530128, 8.659560562354868763E-17, -0.7071067811865421326 ) ) ;
#2445=DIRECTION ( 'NONE',  ( -1.000000000000000000, -0.000000000000000000, -0.000000000000000000 ) ) ;
#2456=CARTESIAN_POINT ( 'NONE',  ( 6.362374563307939823, 3.415000007733389076, 4.302769906042884784 ) ) ;
#2473=EDGE_LOOP ( 'NONE', ( #8167, #11481, #1970, #29 ) ) ;
#2477=( BOUNDED_SURFACE ( )  B_SPLINE_SURFACE ( 3, 2, ( 
 ( #11622, #7349, #5212 ),
 ( #2136, #10511, #4154 ),
 ( #2007, #5273, #4290 ),
 ( #11561, #5408, #4093 ),
 ( #69, #8378, #2201 ),
 ( #13543, #8314, #6445 ) ),
 .UNSPECIFIED., .F., .F., .T. ) 
 B_SPLINE_SURFACE_WITH_KNOTS ( ( 4, 2, 4 ),
 ( 3, 3 ),
 ( 0.02367865728600888897, 0.02663179453327094853, 0.02958493178053300809 ),
 ( 0.000000000000000000, 1.000000000000000000 ),
 .UNSPECIFIED. ) 
 GEOMETRIC_REPRESENTATION_ITEM ( )  RATIONAL_B_SPLINE_SURFACE ( (
 ( 1.000000000000000000, 0.8047781103519399126, 1.000000000000000000),
 ( 1.000000000000000000, 0.8123785825980039954, 1.000000000000000000),
 ( 1.000000000000000000, 0.8190671539288042480, 1.000000000000000000),
 ( 1.000000000000000000, 0.8192352255335092481, 1.000000000000000000),
 ( 1.000000000000000000, 0.8126129676835893711, 1.000000000000000000),
 ( 1.000000000000000000, 0.8047712537969730073, 1.000000000000000000) ) ) 
 REPRESENTATION_ITEM ( '' )  SURFACE ( )  );
#2507=CARTESIAN_POINT ( 'NONE',  ( 0.4465819873849485311, -2.886751345948517677, -5.000000000000000000 ) ) ;
#2540=EDGE_CURVE ( 'NONE', #10855, #3640, #5783, .T. ) ;
#2559=CARTESIAN_POINT ( 'NONE',  ( 6.371506350351443970, 3.439339428956429856, -4.260454149911179655 ) ) ;
#2584=CARTESIAN_POINT ( 'NONE',  ( 6.270568613849413886, 4.911887854652841057, 1.704496029161937320 ) ) ;
#2598=CARTESIAN_POINT ( 'NONE',  ( 6.357965579934049316, -1.995168835099641713, -5.108766517442258959 ) ) ;
#2612=CARTESIAN_POINT ( 'NONE',  ( 6.367873360227558344, -2.886751345948133984, -5.000000000000000000 ) ) ;
#2619=AXIS2_PLACEMENT_3D ( 'NONE', #6603, #9844, #1321 ) ;
#2620=ORIENTED_EDGE ( 'NONE', *, *, #5080, .T. ) ;
#2667=CARTESIAN_POINT ( 'NONE',  ( 6.207530437345011087, 3.810448612249821565, 3.400109403952575882 ) ) ;
#2679=DIRECTION ( 'NONE',  ( -1.000000000000000000, -0.000000000000000000, -0.000000000000000000 ) ) ;
#2681=CARTESIAN_POINT ( 'NONE',  ( 6.445379721942640749, -2.463581311471618740, -5.110653333236677476 ) ) ;
#2685=CARTESIAN_POINT ( 'NONE',  ( 6.533910050139696502, -2.950514251728084236, -5.110440592449055686 ) ) ;
#2694=ORIENTED_EDGE ( 'NONE', *, *, #2540, .F. ) ;
#2749=AXIS2_PLACEMENT_3D ( 'NONE', #12637, #10221, #13386 ) ;
#2772=CARTESIAN_POINT ( 'NONE',  ( 5.991014884144048480, 2.818925648462311528E-15, 4.999999999999999112 ) ) ;
#2783=EDGE_CURVE ( 'NONE', #4363, #9971, #12986, .T. ) ;
#2786=ORIENTED_EDGE ( 'NONE', *, *, #13281, .F. ) ;
#2788=EDGE_CURVE ( 'NONE', #11948, #6035, #13148, .T. ) ;
#2790=CARTESIAN_POINT ( 'NONE',  ( 0.05140428708382594608, 3.841181488860376358, -3.346878500200759277 ) ) ;
#2799=CARTESIAN_POINT ( 'NONE',  ( 6.371919382990604674, 1.972754410575522588, 5.108792907957607099 ) ) ;
#2809=CARTESIAN_POINT ( 'NONE',  ( 6.092449800118089343, 3.827241605637482724, -3.371023086194387286 ) ) ;
#2810=CARTESIAN_POINT ( 'NONE',  ( 6.390820841722131718, -2.823237767533154141, -5.110008744785255352 ) ) ;
#2822=ORIENTED_EDGE ( 'NONE', *, *, #2051, .F. ) ;
#2837=ORIENTED_EDGE ( 'NONE', *, *, #7332, .T. ) ;
#2861=EDGE_CURVE ( 'NONE', #12021, #6051, #7411, .T. ) ;
#2876=CARTESIAN_POINT ( 'NONE',  ( 6.212068001623061164, -3.310128279683368202, -4.266689640017852447 ) ) ;
#2881=CARTESIAN_POINT ( 'NONE',  ( 6.506892073925696351, 2.992473431090949543, -5.000000000000000000 ) ) ;
#2889=TOROIDAL_SURFACE ( 'NONE', #11502, 7.900000000000002132, 0.5999999999999979794 ) ;
#2929=CIRCLE ( 'NONE', #3589, 4.999999999999999112 ) ;
#2951=SHAPE_REPRESENTATION_RELATIONSHIP ( 'NONE' , 'NONE' ,  #9196, #870 ) ;
#2953=DIRECTION ( 'NONE',  ( -1.000000000000000000, -0.000000000000000000, -0.000000000000000000 ) ) ;
#2995=ORIENTED_EDGE ( 'NONE', *, *, #2540, .T. ) ;
#3017=CARTESIAN_POINT ( 'NONE',  ( 6.204460410672268722, 3.831267809383005041, -3.364049496745006529 ) ) ;
#3019=( NAMED_UNIT ( * ) SI_UNIT ( $, .STERADIAN. ) SOLID_ANGLE_UNIT ( ) );
#3048=CARTESIAN_POINT ( 'NONE',  ( 0.000000000000000000, 0.000000000000000000, 0.000000000000000000 ) ) ;
#3057=ORIENTED_EDGE ( 'NONE', *, *, #7332, .F. ) ;
#3086=CARTESIAN_POINT ( 'NONE',  ( 6.506891485183659896, -2.992470280394939675, 5.000000000000000000 ) ) ;
#3087=( NAMED_UNIT ( * ) PLANE_ANGLE_UNIT ( ) SI_UNIT ( $, .RADIAN. ) );
#3116=CARTESIAN_POINT ( 'NONE',  ( 6.355827204229362870, -3.436818823786764288, -4.264647808192651546 ) ) ;
#3146=ADVANCED_FACE ( 'NONE', ( #5767 ), #9967, .T. ) ;
#3149=DIRECTION ( 'NONE',  ( 0.000000000000000000, 0.000000000000000000, 1.000000000000000000 ) ) ;
#3150=ADVANCED_FACE ( 'NONE', ( #682 ), #8240, .T. ) ;
#3151=ORIENTED_EDGE ( 'NONE', *, *, #5779, .T. ) ;
#3193=AXIS2_PLACEMENT_3D ( 'NONE', #6554, #10755, #5454 ) ;
#3213=DIRECTION ( 'NONE',  ( 0.000000000000000000, 0.000000000000000000, 1.000000000000000000 ) ) ;
#3219=FACE_OUTER_BOUND ( 'NONE', #7190, .T. ) ;
#3229=CARTESIAN_POINT ( 'NONE',  ( 6.367873360227559232, -5.773502691896263528, 0.000000000000000000 ) ) ;
#3254=CARTESIAN_POINT ( 'NONE',  ( 6.367873360227558344, 5.773502691896261751, 0.000000000000000000 ) ) ;
#3274=CARTESIAN_POINT ( 'NONE',  ( 6.355324643801635531, -1.972141403783270075, 5.108685331087992942 ) ) ;
#3293=CARTESIAN_POINT ( 'NONE',  ( 6.436591462021358012, -5.789018756751932671, 5.527293451046372024E-16 ) ) ;
#3318=VERTEX_POINT ( 'NONE', #11889 ) ;
#3341=VECTOR ( 'NONE', #10824, 1000.000000000000000 ) ;
#3350=CARTESIAN_POINT ( 'NONE',  ( 6.506987859255518813, 2.925375531177291766, 5.066899051217865768 ) ) ;
#3356=CARTESIAN_POINT ( 'NONE',  ( 0.000000000000000000, 0.000000000000000000, 0.000000000000000000 ) ) ;
#3360=CARTESIAN_POINT ( 'NONE',  ( 6.534533895392296010, -5.902695350657468865, 6.631005141235907328E-15 ) ) ;
#3370=CARTESIAN_POINT ( 'NONE',  ( 0.000000000000000000, -4.330127018922188320, 2.500000000000010214 ) ) ;
#3387=B_SPLINE_CURVE_WITH_KNOTS ( 'NONE', 3,
 ( #618, #826, #7226, #12533 ),
 .UNSPECIFIED., .F., .F.,
 ( 4, 4 ),
 ( 2.380735200831296902E-07, 0.002921158011986723767 ),
 .UNSPECIFIED. ) ;
#3396=ADVANCED_FACE ( 'NONE', ( #5414 ), #10779, .F. ) ;
#3404=DIRECTION ( 'NONE',  ( -1.000000000000000000, -0.000000000000000000, -0.000000000000000000 ) ) ;
#3411=CARTESIAN_POINT ( 'NONE',  ( 6.367873360227558344, 5.773502691896261751, 0.000000000000000000 ) ) ;
#3420=CARTESIAN_POINT ( 'NONE',  ( 7.336184427528458230, 0.000000000000000000, 0.000000000000000000 ) ) ;
#3433=CARTESIAN_POINT ( 'NONE',  ( 0.4465819873852049926, -5.773502691896263528, -3.127607256515468906E-17 ) ) ;
#3437=CARTESIAN_POINT ( 'NONE',  ( 6.367873360227555679, -2.886751345948119774, 4.999999999999999112 ) ) ;
#3449=EDGE_LOOP ( 'NONE', ( #988, #12456 ) ) ;
#3471=DIRECTION ( 'NONE',  ( 1.000000000000000000, 0.000000000000000000, 0.000000000000000000 ) ) ;
#3472=CARTESIAN_POINT ( 'NONE',  ( 0.000000000000000000, 0.000000000000000000, 5.000000000000000000 ) ) ;
#3477=LINE ( 'NONE', #4444, #5569 ) ;
#3526=PRODUCT_DEFINITION_FORMATION_WITH_SPECIFIED_SOURCE ( 'ANY', '', #11047, .NOT_KNOWN. ) ;
#3551=EDGE_CURVE ( 'NONE', #6051, #844, #4578, .T. ) ;
#3553=CARTESIAN_POINT ( 'NONE',  ( 6.367873360227556567, 2.886751345948125991, 4.999999999999999112 ) ) ;
#3589=AXIS2_PLACEMENT_3D ( 'NONE', #9032, #13231, #3776 ) ;
#3593=CARTESIAN_POINT ( 'NONE',  ( 7.336184427528458230, 0.000000000000000000, -8.105212085995399107 ) ) ;
#3605=ORIENTED_EDGE ( 'NONE', *, *, #6787, .T. ) ;
#3606=ORIENTED_EDGE ( 'NONE', *, *, #5620, .T. ) ;
#3607=CARTESIAN_POINT ( 'NONE',  ( 6.445127866599365873, 3.194847394660948581, -4.687657648742338701 ) ) ;
#3624=CARTESIAN_POINT ( 'NONE',  ( 0.000000000000000000, 0.000000000000000000, 0.000000000000000000 ) ) ;
#3638=AXIS2_PLACEMENT_3D ( 'NONE', #9573, #12736, #7501 ) ;
#3640=VERTEX_POINT ( 'NONE', #9199 ) ;
#3645=CARTESIAN_POINT ( 'NONE',  ( 8.500000000000000000, -5.773502691896263528, 0.000000000000000000 ) ) ;
#3648=CARTESIAN_POINT ( 'NONE',  ( 6.242811304425483598, -0.9953138271174254426, -5.105233480330447549 ) ) ;
#3671=ORIENTED_EDGE ( 'NONE', *, *, #13281, .T. ) ;
#3682=CARTESIAN_POINT ( 'NONE',  ( 0.000000000000000000, 0.000000000000000000, 0.000000000000000000 ) ) ;
#3695=CARTESIAN_POINT ( 'NONE',  ( 6.271006797790669829, 0.9853839345309320930, 5.106080050406710313 ) ) ;
#3719=AXIS2_PLACEMENT_3D ( 'NONE', #7726, #5585, #12072 ) ;
#3735=ORIENTED_EDGE ( 'NONE', *, *, #8148, .F. ) ;
#3762=DIRECTION ( 'NONE',  ( 0.000000000000000000, 0.000000000000000000, 1.000000000000000000 ) ) ;
#3775=CARTESIAN_POINT ( 'NONE',  ( 6.390983399715594260, -5.837459000499769957, 0.1107755759658282380 ) ) ;
#3776=DIRECTION ( 'NONE',  ( 0.000000000000000000, 0.000000000000000000, -1.000000000000000000 ) ) ;
#3791=CIRCLE ( 'NONE', #1346, 3.309499999999999886 ) ;
#3795=FACE_OUTER_BOUND ( 'NONE', #10680, .T. ) ;
#3804=ORIENTED_EDGE ( 'NONE', *, *, #13028, .T. ) ;
#3811=EDGE_CURVE ( 'NONE', #13345, #1735, #5259, .T. ) ;
#3813=DIRECTION ( 'NONE',  ( 0.000000000000000000, 0.000000000000000000, 1.000000000000000000 ) ) ;
#3825=ORIENTED_EDGE ( 'NONE', *, *, #12932, .F. ) ;
#3827=ORIENTED_EDGE ( 'NONE', *, *, #6073, .F. ) ;
#3828=PLANE ( 'NONE',  #8709 ) ;
#3854=AXIS2_PLACEMENT_3D ( 'NONE', #3048, #5213, #13613 ) ;
#3872=B_SPLINE_CURVE_WITH_KNOTS ( 'NONE', 3,
 ( #1884, #6195, #12461, #2790, #8189, #11362, #4107, #4944 ),
 .UNSPECIFIED., .F., .F.,
 ( 4, 2, 2, 4 ),
 ( 0.002921158011986723767, 0.003648658599403076588, 0.004376159186819428976, 0.005831160361652133750 ),
 .UNSPECIFIED. ) ;
#3876=CARTESIAN_POINT ( 'NONE',  ( 0.000000000000000000, -4.330127018922193649, -2.500000000000000000 ) ) ;
#3880=DIRECTION ( 'NONE',  ( 1.000000000000000000, 0.000000000000000000, 0.000000000000000000 ) ) ;
#3911=CARTESIAN_POINT ( 'NONE',  ( 6.207671477328021048, 3.321994320370322828, -4.246137054663353005 ) ) ;
#3914=FACE_OUTER_BOUND ( 'NONE', #5671, .T. ) ;
#3924=EDGE_CURVE ( 'NONE', #10124, #13345, #5626, .T. ) ;
#3932=DIRECTION ( 'NONE',  ( 1.000000000000000000, 0.000000000000000000, 0.000000000000000000 ) ) ;
#3974=ORIENTED_EDGE ( 'NONE', *, *, #8638, .T. ) ;
#3975=CARTESIAN_POINT ( 'NONE',  ( 52.80949999999998568, 4.898587196589412829E-16, -4.000000000000000000 ) ) ;
#3988=EDGE_CURVE ( 'NONE', #9307, #6035, #1401, .T. ) ;
#3995=VECTOR ( 'NONE', #4490, 1000.000000000000000 ) ;
#4011=ORIENTED_EDGE ( 'NONE', *, *, #5779, .F. ) ;
#4019=CARTESIAN_POINT ( 'NONE',  ( 6.270568613849419215, -4.911887854652846386, -1.704496029161938875 ) ) ;
#4029=VERTEX_POINT ( 'NONE', #1823 ) ;
#4034=CARTESIAN_POINT ( 'NONE',  ( 6.518095160331716542, 5.866179305615093043, 1.445124054326800857E-15 ) ) ;
#4037=CARTESIAN_POINT ( 'NONE',  ( 8.500000000000000000, 2.886751345948123770, -5.000000000000000000 ) ) ;
#4064=ORIENTED_EDGE ( 'NONE', *, *, #6440, .F. ) ;
#4093=CARTESIAN_POINT ( 'NONE',  ( 6.242800618755128816, -3.923709308886856206, 3.414402460854895072 ) ) ;
#4101=ORIENTED_EDGE ( 'NONE', *, *, #11505, .T. ) ;
#4106=PLANE ( 'NONE',  #2157 ) ;
#4107=CARTESIAN_POINT ( 'NONE',  ( 0.3106000600989267113, 3.122278952918445150, -4.592054218142293642 ) ) ;
#4132=CARTESIAN_POINT ( 'NONE',  ( 6.196878017913830305, -3.367876570272811509, 4.166666666666666963 ) ) ;
#4144=CARTESIAN_POINT ( 'NONE',  ( 6.534838248920900483, -5.903531555104836848, 4.671345613696493211E-16 ) ) ;
#4153=CARTESIAN_POINT ( 'NONE',  ( 7.900000000000002132, 9.674709713264094059E-16, -7.900000000000002132 ) ) ;
#4154=CARTESIAN_POINT ( 'NONE',  ( 6.362374563307726660, -5.433808049138435514, 0.8060918076010795685 ) ) ;
#4155=CARTESIAN_POINT ( 'NONE',  ( 6.244297270354684848, -1.798312406574552930E-11, -5.105276777067894400 ) ) ;
#4168=CARTESIAN_POINT ( 'NONE',  ( 6.481779955677436256, 5.820445026626583918, -1.884471986315529758E-16 ) ) ;
#4169=ADVANCED_FACE ( 'NONE', ( #7092, #1540 ), #12134, .T. ) ;
#4187=COLOUR_RGB ( '',1.000000000000000000, 0.9490196078431372140, 0.9098039215686274384 ) ;
#4190=CARTESIAN_POINT ( 'NONE',  ( 6.534533895392294234, 2.951347675328725106, 5.111884124469659341 ) ) ;
#4217=ORIENTED_EDGE ( 'NONE', *, *, #6291, .T. ) ;
#4235=DIRECTION ( 'NONE',  ( -0.000000000000000000, 0.000000000000000000, -1.000000000000000000 ) ) ;
#4251=B_SPLINE_CURVE_WITH_KNOTS ( 'NONE', 3,
 ( #2507, #12239, #1387, #3876 ),
 .UNSPECIFIED., .F., .F.,
 ( 4, 4 ),
 ( 2.380735203086575858E-07, 0.002921158011986710323 ),
 .UNSPECIFIED. ) ;
#4257=CARTESIAN_POINT ( 'NONE',  ( 6.452281807715809059, 2.898928808472990060, 5.021091983800332947 ) ) ;
#4290=CARTESIAN_POINT ( 'NONE',  ( 6.245824673232967861, -4.939548505213401164, 1.655093584844986143 ) ) ;
#4299=CIRCLE ( 'NONE', #3854, 4.999999999999999112 ) ;
#4302=EDGE_LOOP ( 'NONE', ( #2837, #12907, #1371, #5774, #13187 ) ) ;
#4305=CARTESIAN_POINT ( 'NONE',  ( 6.506987859255521478, 5.850751062354592413, 1.196609732200561596E-15 ) ) ;
#4318=FACE_OUTER_BOUND ( 'NONE', #2263, .T. ) ;
#4319=ORIENTED_EDGE ( 'NONE', *, *, #5252, .T. ) ;
#4363=VERTEX_POINT ( 'NONE', #13573 ) ;
#4384=CIRCLE ( 'NONE', #2383, 4.000000000000000000 ) ;
#4390=ADVANCED_FACE ( 'NONE', ( #4318 ), #11709, .F. ) ;
#4393=CARTESIAN_POINT ( 'NONE',  ( 6.534838248920900483, -5.903531555104836848, 4.671345613696493211E-16 ) ) ;
#4395=CARTESIAN_POINT ( 'NONE',  ( 0.08165819712377191120, -4.939961795957299451, -1.443735181952766400 ) ) ;
#4444=CARTESIAN_POINT ( 'NONE',  ( 8.500000000000000000, 2.886751345948125991, 4.999999999999999112 ) ) ;
#4451=CARTESIAN_POINT ( 'NONE',  ( 6.534838248920897819, 2.951765777552412651, 5.112608298763836601 ) ) ;
#4466=CARTESIAN_POINT ( 'NONE',  ( 0.3106000600989309857, -5.537975084925943037, -0.4079457818577079120 ) ) ;
#4473=CARTESIAN_POINT ( 'NONE',  ( 0.01055556052338869899, -4.084588180558399451, 2.925285743277528105 ) ) ;
#4490=DIRECTION ( 'NONE',  ( -1.000000000000000000, -0.000000000000000000, -0.000000000000000000 ) ) ;
#4533=CARTESIAN_POINT ( 'NONE',  ( 0.4465819873852006072, 2.886751345948123770, -5.000000000000000000 ) ) ;
#4536=CARTESIAN_POINT ( 'NONE',  ( -7.092489211676000613E-16, -4.452621892014641425, -2.287832656137186671 ) ) ;
#4537=EDGE_LOOP ( 'NONE', ( #13176, #3606, #8862, #7020 ) ) ;
#4570=EDGE_LOOP ( 'NONE', ( #9375, #6850, #3804 ) ) ;
#4578=B_SPLINE_CURVE_WITH_KNOTS ( 'NONE', 3,
 ( #6916, #10015, #532, #8988, #10981 ),
 .UNSPECIFIED., .F., .F.,
 ( 4, 1, 4 ),
 ( 0.000000000000000000, 0.002886751345948128985, 0.005773502691896257970 ),
 .UNSPECIFIED. ) ;
#4590=B_SPLINE_CURVE_WITH_KNOTS ( 'NONE', 3,
 ( #12873, #13262, #2772, #2367, #3553 ),
 .UNSPECIFIED., .F., .F.,
 ( 4, 1, 4 ),
 ( 0.000000000000000000, 0.002886751345948122913, 0.005773502691896245827 ),
 .UNSPECIFIED. ) ;
#4639=ORIENTED_EDGE ( 'NONE', *, *, #11441, .T. ) ;
#4644=ORIENTED_EDGE ( 'NONE', *, *, #52, .T. ) ;
#4645=CARTESIAN_POINT ( 'NONE',  ( 6.270568613849413886, 3.932080789230360196, -3.401571648088637101 ) ) ;
#4647=EDGE_CURVE ( 'NONE', #5390, #10855, #9672, .T. ) ;
#4675=UNCERTAINTY_MEASURE_WITH_UNIT (LENGTH_MEASURE( 1.000000000000000082E-05 ), #9384, 'distance_accuracy_value', 'NONE');
#4696=CARTESIAN_POINT ( 'NONE',  ( 0.000000000000000000, 4.898587196589412829E-16, -4.000000000000000000 ) ) ;
#4716=AXIS2_PLACEMENT_3D ( 'NONE', #8140, #2953, #7029 ) ;
#4737=CONICAL_SURFACE ( 'NONE', #303, 5.000000000000000000, 1.047197551196600296 ) ;
#4742=DIRECTION ( 'NONE',  ( -1.000000000000000000, -0.000000000000000000, -0.000000000000000000 ) ) ;
#4746=ORIENTED_EDGE ( 'NONE', *, *, #8633, .T. ) ;
#4747=CARTESIAN_POINT ( 'NONE',  ( 0.4465819873849485311, -2.886751345948517677, -5.000000000000000000 ) ) ;
#4751=( LENGTH_UNIT ( ) NAMED_UNIT ( * ) SI_UNIT ( .MILLI., .METRE. ) );
#4769=CARTESIAN_POINT ( 'NONE',  ( 6.534838248920899595, -2.951765777552420644, -5.112608298763837489 ) ) ;
#4816=CARTESIAN_POINT ( 'NONE',  ( 6.385552186430388133, -2.886751345948118441, 5.000000000000000888 ) ) ;
#4850=LINE ( 'NONE', #5894, #12774 ) ;
#4876=( BOUNDED_SURFACE ( )  B_SPLINE_SURFACE ( 3, 2, ( 
 ( #5870, #2881, #1763 ),
 ( #7103, #11312, #13167 ),
 ( #1834, #6083, #8909 ),
 ( #9036, #13104, #3648 ),
 ( #7870, #12079, #2598 ),
 ( #6826, #1551, #11032 ) ),
 .UNSPECIFIED., .F., .F., .T. ) 
 B_SPLINE_SURFACE_WITH_KNOTS ( ( 4, 2, 4 ),
 ( 3, 3 ),
 ( 0.02368235114939812314, 0.02663560780161266378, 0.02958886445382720443 ),
 ( 0.000000000000000000, 1.000000000000000000 ),
 .UNSPECIFIED. ) 
 GEOMETRIC_REPRESENTATION_ITEM ( )  RATIONAL_B_SPLINE_SURFACE ( (
 ( 1.000000000000000000, 0.8047780980783513227, 1.000000000000000000),
 ( 1.000000000000000000, 0.8123789398383446381, 1.000000000000000000),
 ( 1.000000000000000000, 0.8190677725692530053, 1.000000000000000000),
 ( 1.000000000000000000, 0.8192346316605858547, 1.000000000000000000),
 ( 1.000000000000000000, 0.8126126875065289301, 1.000000000000000000),
 ( 1.000000000000000000, 0.8047712635281869531, 1.000000000000000000) ) ) 
 REPRESENTATION_ITEM ( '' )  SURFACE ( )  );
#4889=CARTESIAN_POINT ( 'NONE',  ( 6.204460410672267834, -4.828986228461502606, -1.635950503254466337 ) ) ;
#4914=B_SPLINE_CURVE_WITH_KNOTS ( 'NONE', 3,
 ( #12940, #6672, #10872, #599 ),
 .UNSPECIFIED., .F., .F.,
 ( 4, 4 ),
 ( 2.380735200829041677E-07, 0.002921158011986707288 ),
 .UNSPECIFIED. ) ;
#4937=ADVANCED_FACE ( 'NONE', ( #5089 ), #48, .T. ) ;
#4944=CARTESIAN_POINT ( 'NONE',  ( 0.4465819873852006072, 2.886751345948123770, -5.000000000000000000 ) ) ;
#4961=B_SPLINE_CURVE_WITH_KNOTS ( 'NONE', 3,
 ( #1796, #6044, #11134, #5762, #12110, #8033 ),
 .UNSPECIFIED., .F., .F.,
 ( 4, 2, 4 ),
 ( 0.005339748439308726613, 0.006800846765732536554, 0.008261945092156346496 ),
 .UNSPECIFIED. ) ;
#4963=CARTESIAN_POINT ( 'NONE',  ( 6.207671477328757348, -5.338259717474211463, -0.7538629453363940858 ) ) ;
#4969=AXIS2_PLACEMENT_3D ( 'NONE', #1894, #12546, #8342 ) ;
#4980=CARTESIAN_POINT ( 'NONE',  ( 6.534838248920900483, -5.903531555104836848, 4.671345613696493211E-16 ) ) ;
#4985=CARTESIAN_POINT ( 'NONE',  ( 5.991014884144048480, 4.330127018922193649, 2.500000000000001776 ) ) ;
#5005=CONICAL_SURFACE ( 'NONE', #12712, 3.309499999999999886, 0.7853981633974407295 ) ;
#5016=DIRECTION ( 'NONE',  ( -1.000000000000000000, -0.000000000000000000, -0.000000000000000000 ) ) ;
#5033=CARTESIAN_POINT ( 'NONE',  ( 6.534838248920896930, -2.951765777552406878, 5.112608298763836601 ) ) ;
#5080=EDGE_CURVE ( 'NONE', #6586, #9257, #11873, .T. ) ;
#5082=CARTESIAN_POINT ( 'NONE',  ( 6.495567275915080430, 5.834887664329775347, 9.410860448829699171E-16 ) ) ;
#5089=FACE_OUTER_BOUND ( 'NONE', #7593, .T. ) ;
#5119=ORIENTED_EDGE ( 'NONE', *, *, #11441, .F. ) ;
#5145=AXIS2_PLACEMENT_3D ( 'NONE', #8466, #9500, #3213 ) ;
#5156=CARTESIAN_POINT ( 'NONE',  ( 0.000000000000000000, 5.773502691896261751, -2.749426538070115714E-16 ) ) ;
#5175=CARTESIAN_POINT ( 'NONE',  ( 6.362374563308228481, 5.433808049139812191, -0.8060918076009558897 ) ) ;
#5176=CARTESIAN_POINT ( 'NONE',  ( 6.207530437345013752, -3.810448612250145750, -3.400109403952246367 ) ) ;
#5193=DIRECTION ( 'NONE',  ( 1.000000000000000000, 0.000000000000000000, 0.000000000000000000 ) ) ;
#5212=CARTESIAN_POINT ( 'NONE',  ( 6.541171661047877173, -5.920857802016179505, -0.02973393389965061501 ) ) ;
#5213=DIRECTION ( 'NONE',  ( 1.000000000000000000, 0.000000000000000000, -0.000000000000000000 ) ) ;
#5223=CARTESIAN_POINT ( 'NONE',  ( 6.436591462021357124, 5.789018756751930894, -2.883547477572278442E-16 ) ) ;
#5224=CARTESIAN_POINT ( 'NONE',  ( 6.436591462021363341, 2.894509378375959674, -5.013437306331780086 ) ) ;
#5228=EDGE_CURVE ( 'NONE', #6586, #6035, #8671, .T. ) ;
#5231=CARTESIAN_POINT ( 'NONE',  ( 6.244297270354683960, 1.802013835206515036E-11, 5.105276777067893512 ) ) ;
#5238=DIRECTION ( 'NONE',  ( 0.000000000000000000, 0.5000000000000018874, 0.8660254037844375974 ) ) ;
#5239=ORIENTED_EDGE ( 'NONE', *, *, #12441, .T. ) ;
#5241=CARTESIAN_POINT ( 'NONE',  ( 6.466260427357663154, 2.904280683598005730, 5.030361703432624232 ) ) ;
#5244=CARTESIAN_POINT ( 'NONE',  ( 6.327640840229819652, -2.033197012992983943, 4.999999999998298250 ) ) ;
#5248=CARTESIAN_POINT ( 'NONE',  ( 6.196878017913831194, -5.292377467571572680, 0.8333333333333327042 ) ) ;
#5252=EDGE_CURVE ( 'NONE', #5998, #7289, #3477, .T. ) ;
#5259=B_SPLINE_CURVE_WITH_KNOTS ( 'NONE', 3,
 ( #1399, #4536, #9789, #6493, #4395, #9724, #4466, #3433 ),
 .UNSPECIFIED., .F., .F.,
 ( 4, 2, 2, 4 ),
 ( 0.002921158011986710323, 0.003648658599403064445, 0.004376159186819419435, 0.005831160361652128546 ),
 .UNSPECIFIED. ) ;
#5273=CARTESIAN_POINT ( 'NONE',  ( 6.207530437345012864, -4.849805425595699937, 1.599890596045217439 ) ) ;
#5286=CARTESIAN_POINT ( 'NONE',  ( 6.534533895392296010, 5.902695350657467088, 5.075181882648644095E-15 ) ) ;
#5353=CARTESIAN_POINT ( 'NONE',  ( 0.000000000000000000, -4.330127018922188320, 2.500000000000010214 ) ) ;
#5365=CARTESIAN_POINT ( 'NONE',  ( 6.367873360227556567, 2.886751345948123770, -5.000000000000000000 ) ) ;
#5369=ORIENTED_EDGE ( 'NONE', *, *, #2861, .T. ) ;
#5373=CARTESIAN_POINT ( 'NONE',  ( 6.495567275915077765, 2.917443832164883233, 5.053160945538031079 ) ) ;
#5390=VERTEX_POINT ( 'NONE', #1997 ) ;
#5408=CARTESIAN_POINT ( 'NONE',  ( 6.204460410672268722, -3.831267809382561840, 3.364049496746113199 ) ) ;
#5414=FACE_OUTER_BOUND ( 'NONE', #6739, .T. ) ;
#5443=CARTESIAN_POINT ( 'NONE',  ( 52.80949999999998568, 0.000000000000000000, 4.000000000000000000 ) ) ;
#5451=CARTESIAN_POINT ( 'NONE',  ( 6.244889965166094292, 3.924082311521017274, 3.413878157001050795 ) ) ;
#5454=DIRECTION ( 'NONE',  ( 0.000000000000000000, 0.000000000000000000, -1.000000000000000000 ) ) ;
#5480=VERTEX_POINT ( 'NONE', #13271 ) ;
#5498=ORIENTED_EDGE ( 'NONE', *, *, #11044, .T. ) ;
#5524=CARTESIAN_POINT ( 'NONE',  ( 0.000000000000000000, 0.000000000000000000, -5.000000000000000000 ) ) ;
#5546=ORIENTED_EDGE ( 'NONE', *, *, #11849, .T. ) ;
#5547=ORIENTED_EDGE ( 'NONE', *, *, #5704, .F. ) ;
#5552=CARTESIAN_POINT ( 'NONE',  ( 0.1996310553826632361, 1.947030205581113282, 4.999999999999997335 ) ) ;
#5569=VECTOR ( 'NONE', #6732, 1000.000000000000000 ) ;
#5578=CARTESIAN_POINT ( 'NONE',  ( 7.336184427528458230, 0.000000000000000000, 0.000000000000000000 ) ) ;
#5585=DIRECTION ( 'NONE',  ( 0.000000000000000000, 0.000000000000000000, -1.000000000000000000 ) ) ;
#5619=CARTESIAN_POINT ( 'NONE',  ( 53.50000000000000000, 4.052968581778165278E-16, -3.309499999999999886 ) ) ;
#5620=EDGE_CURVE ( 'NONE', #11251, #11948, #7771, .T. ) ;
#5623=MANIFOLD_SOLID_BREP ( 'FlangeHexFillet', #11330 ) ;
#5626=CIRCLE ( 'NONE', #3193, 4.999999999999999112 ) ;
#5632=AXIS2_PLACEMENT_3D ( 'NONE', #12910, #12975, #9746 ) ;
#5637=FACE_OUTER_BOUND ( 'NONE', #11689, .T. ) ;
#5641=CARTESIAN_POINT ( 'NONE',  ( 6.242789945155967857, 0.9948955795114693412, 5.105232858000414708 ) ) ;
#5659=CARTESIAN_POINT ( 'NONE',  ( 6.507056315241515954, 5.826803161468471437, -0.09231912136634902455 ) ) ;
#5671=EDGE_LOOP ( 'NONE', ( #1487, #1663, #4064, #2001 ) ) ;
#5704=EDGE_CURVE ( 'NONE', #12356, #5390, #1160, .T. ) ;
#5707=CARTESIAN_POINT ( 'NONE',  ( 6.390983631292896483, 3.014665224428355383, 4.999999999999999112 ) ) ;
#5721=DIRECTION ( 'NONE',  ( 0.000000000000000000, 0.000000000000000000, -1.000000000000000000 ) ) ;
#5723=B_SPLINE_CURVE_WITH_KNOTS ( 'NONE', 3,
 ( #5740, #2681, #9120, #12088, #9941, #11113 ),
 .UNSPECIFIED., .F., .F.,
 ( 4, 2, 4 ),
 ( 4.336808689942017736E-19, 0.001488912493401929995, 0.002977824986803859555 ),
 .UNSPECIFIED. ) ;
#5727=CARTESIAN_POINT ( 'NONE',  ( 6.357976367241986893, 5.421935536069748096, 0.8264656814052228073 ) ) ;
#5735=ORIENTED_EDGE ( 'NONE', *, *, #325, .T. ) ;
#5736=VERTEX_POINT ( 'NONE', #2378 ) ;
#5740=CARTESIAN_POINT ( 'NONE',  ( 6.534838248920899595, -2.951765777552420644, -5.112608298763837489 ) ) ;
#5756=CARTESIAN_POINT ( 'NONE',  ( 6.355827204229362870, 5.411702751981843917, -0.8440485055075606091 ) ) ;
#5761=CARTESIAN_POINT ( 'NONE',  ( 0.04320752586819863461, 0.9836842030436160345, 4.999999999999999112 ) ) ;
#5762=CARTESIAN_POINT ( 'NONE',  ( 0.04201760816083378175, -0.9730571234388133428, 4.999999999999997335 ) ) ;
#5767=FACE_OUTER_BOUND ( 'NONE', #2473, .T. ) ;
#5773=EDGE_CURVE ( 'NONE', #3318, #8372, #6391, .T. ) ;
#5774=ORIENTED_EDGE ( 'NONE', *, *, #11276, .F. ) ;
#5779=EDGE_CURVE ( 'NONE', #6035, #9307, #2395, .T. ) ;
#5783=LINE ( 'NONE', #6877, #6989 ) ;
#5791=UNCERTAINTY_MEASURE_WITH_UNIT (LENGTH_MEASURE( 1.000000000000000082E-05 ), #4751, 'distance_accuracy_value', 'NONE');
#5812=AXIS2_PLACEMENT_3D ( 'NONE', #3682, #13002, #1589 ) ;
#5816=CARTESIAN_POINT ( 'NONE',  ( 6.196878017913833858, 5.292377467571573568, 0.8333333333333322601 ) ) ;
#5828=CARTESIAN_POINT ( 'NONE',  ( 0.000000000000000000, 0.000000000000000000, 0.000000000000000000 ) ) ;
#5867=CARTESIAN_POINT ( 'NONE',  ( 6.242800618755108388, 4.918813924286816963, 1.690830708135752758 ) ) ;
#5870=CARTESIAN_POINT ( 'NONE',  ( 6.390821132688881967, 3.013780087859769363, -5.000000000000000000 ) ) ;
#5881=PRODUCT_DEFINITION_SHAPE ( 'NONE', 'NONE',  #6587 ) ;
#5894=CARTESIAN_POINT ( 'NONE',  ( 8.500000000000000000, 5.773502691896261751, 0.000000000000000000 ) ) ;
#5910=PLANE ( 'NONE',  #33 ) ;
#5928=CARTESIAN_POINT ( 'NONE',  ( 6.506891779418576327, -2.833891091414761032, -5.091556646552826138 ) ) ;
#5939=VECTOR ( 'NONE', #2679, 1000.000000000000000 ) ;
#5971=AXIS2_PLACEMENT_3D ( 'NONE', #801, #7464, #5193 ) ;
#5982=EDGE_LOOP ( 'NONE', ( #2694, #13577, #4319, #3735, #7270 ) ) ;
#5985=CARTESIAN_POINT ( 'NONE',  ( 53.50000000000000000, 0.000000000000000000, 0.000000000000000000 ) ) ;
#5998=VERTEX_POINT ( 'NONE', #9393 ) ;
#6002=CARTESIAN_POINT ( 'NONE',  ( 6.481779955677443361, -2.910222513313286186, 5.040653254389420468 ) ) ;
#6017=ORIENTED_EDGE ( 'NONE', *, *, #5773, .T. ) ;
#6025=CARTESIAN_POINT ( 'NONE',  ( 6.403457969954082785, -2.888443235695457467, -5.002930439003169916 ) ) ;
#6035=VERTEX_POINT ( 'NONE', #8820 ) ;
#6044=CARTESIAN_POINT ( 'NONE',  ( 0.3108895250735811966, -2.416698868092462149, 4.999999999999999112 ) ) ;
#6051=VERTEX_POINT ( 'NONE', #371 ) ;
#6064=DIRECTION ( 'NONE',  ( -1.000000000000000000, -0.000000000000000000, -0.000000000000000000 ) ) ;
#6066=DIRECTION ( 'NONE',  ( 0.000000000000000000, 0.000000000000000000, 1.000000000000000000 ) ) ;
#6073=EDGE_CURVE ( 'NONE', #8324, #8131, #8920, .T. ) ;
#6077=CARTESIAN_POINT ( 'NONE',  ( 6.507056315241514177, 2.833450876375910976, -5.092319121366348789 ) ) ;
#6079=FILL_AREA_STYLE_COLOUR ( '', #4187 ) ;
#6083=CARTESIAN_POINT ( 'NONE',  ( 6.207519134555854023, 1.039264565631282888, -4.999999999999109157 ) ) ;
#6095=VERTEX_POINT ( 'NONE', #4533 ) ;
#6126=DIRECTION ( 'NONE',  ( -1.000000000000000000, 0.000000000000000000, -0.000000000000000000 ) ) ;
#6127=DIRECTION ( 'NONE',  ( 0.000000000000000000, 0.000000000000000000, 1.000000000000000000 ) ) ;
#6147=CARTESIAN_POINT ( 'NONE',  ( 6.466260427357672036, -2.904280683598005286, 5.030361703432631337 ) ) ;
#6189=ORIENTED_EDGE ( 'NONE', *, *, #12099, .F. ) ;
#6193=CARTESIAN_POINT ( 'NONE',  ( 6.534533895392294234, 2.951347675328729991, -5.111884124469655788 ) ) ;
#6195=CARTESIAN_POINT ( 'NONE',  ( -3.417495597855351487E-15, 4.207632145829744097, -2.712167343862822655 ) ) ;
#6215=ORIENTED_EDGE ( 'NONE', *, *, #10570, .F. ) ;
#6219=EDGE_CURVE ( 'NONE', #8131, #6586, #8264, .T. ) ;
#6220=CARTESIAN_POINT ( 'NONE',  ( 6.541171661047875396, 5.920857802016174176, 0.02973393389964464062 ) ) ;
#6221=CARTESIAN_POINT ( 'NONE',  ( 6.533910050139693837, -2.950514251728023840, 5.110440592449081443 ) ) ;
#6267=CARTESIAN_POINT ( 'NONE',  ( 6.367873360227558344, 5.773502691896261751, 0.000000000000000000 ) ) ;
#6268=DIRECTION ( 'NONE',  ( 1.000000000000000000, 0.000000000000000000, -0.000000000000000000 ) ) ;
#6270=CARTESIAN_POINT ( 'NONE',  ( 0.04320752586819883584, 0.9836842030436125928, -5.000000000000000000 ) ) ;
#6291=EDGE_CURVE ( 'NONE', #486, #11340, #8596, .T. ) ;
#6299=ORIENTED_EDGE ( 'NONE', *, *, #1511, .T. ) ;
#6309=( BOUNDED_SURFACE ( )  B_SPLINE_SURFACE ( 3, 2, ( 
 ( #13579, #8349, #6220 ),
 ( #8207, #12553, #5175 ),
 ( #7316, #8069, #9103 ),
 ( #2809, #3017, #9381 ),
 ( #3911, #9242, #7172 ),
 ( #1829, #6077, #13505 ) ),
 .UNSPECIFIED., .F., .F., .F. ) 
 B_SPLINE_SURFACE_WITH_KNOTS ( ( 4, 2, 4 ),
 ( 3, 3 ),
 ( 0.02367865728600889938, 0.02663179453327095547, 0.02958493178053301503 ),
 ( 0.000000000000000000, 1.000000000000000000 ),
 .UNSPECIFIED. ) 
 GEOMETRIC_REPRESENTATION_ITEM ( )  RATIONAL_B_SPLINE_SURFACE ( (
 ( 1.000000000000000000, 0.8047781103519390244, 1.000000000000000000),
 ( 1.000000000000000000, 0.8123785825980075481, 1.000000000000000000),
 ( 1.000000000000000000, 0.8190671539288042480, 1.000000000000000000),
 ( 1.000000000000000000, 0.8192352255335092481, 1.000000000000000000),
 ( 1.000000000000000000, 0.8126129676835915916, 1.000000000000000000),
 ( 1.000000000000000000, 0.8047712537969718971, 1.000000000000000000) ) ) 
 REPRESENTATION_ITEM ( '' )  SURFACE ( )  );
#6320=FACE_OUTER_BOUND ( 'NONE', #12526, .T. ) ;
#6330=ORIENTED_EDGE ( 'NONE', *, *, #8914, .T. ) ;
#6332=FACE_OUTER_BOUND ( 'NONE', #7796, .T. ) ;
#6334=CARTESIAN_POINT ( 'NONE',  ( -1.575481281892997891E-16, 0.4887495715076908831, -5.000000000000000000 ) ) ;
#6352=CARTESIAN_POINT ( 'NONE',  ( 6.207541730803228575, -1.039448978216581665, 5.000000000000000888 ) ) ;
#6363=ORIENTED_EDGE ( 'NONE', *, *, #5252, .F. ) ;
#6365=CARTESIAN_POINT ( 'NONE',  ( 0.3106000600989247684, -3.122278952918441597, 4.592054218142290978 ) ) ;
#6380=VECTOR ( 'NONE', #2419, 999.9999999999998863 ) ;
#6389=APPLICATION_CONTEXT ( 'automotive_design' ) ;
#6391=CIRCLE ( 'NONE', #1281, 4.000000000000000000 ) ;
#6396=CARTESIAN_POINT ( 'NONE',  ( 6.385552186430389021, 2.886751345948122438, -5.000000000000001776 ) ) ;
#6419=AXIS2_PLACEMENT_3D ( 'NONE', #3356, #2310, #12813 ) ;
#6420=B_SPLINE_CURVE_WITH_KNOTS ( 'NONE', 3,
 ( #9510, #7572, #9441, #10612, #10477, #4257, #5241, #11713, #5373, #3350, #8413, #235, #9577, #12551, #4190, #4451 ),
 .UNSPECIFIED., .F., .F.,
 ( 4, 3, 3, 3, 3, 4 ),
 ( 0.000000000000000000, 5.303647860849292387E-05, 0.0001057093501027219331, 0.0001642058037231606204, 0.0002210073443958821807, 0.0002236769549542877021 ),
 .UNSPECIFIED. ) ;
#6425=CARTESIAN_POINT ( 'NONE',  ( 6.533910050139697390, -5.901028503456124064, 1.992084869049455159E-14 ) ) ;
#6440=EDGE_CURVE ( 'NONE', #11340, #486, #1572, .T. ) ;
#6445=CARTESIAN_POINT ( 'NONE',  ( 6.541334219041335274, -2.934241909852036478, 5.143243597038029691 ) ) ;
#6449=EDGE_CURVE ( 'NONE', #6051, #6095, #981, .T. ) ;
#6457=VECTOR ( 'NONE', #12933, 1000.000000000000114 ) ;
#6462=LINE ( 'NONE', #11766, #6938 ) ;
#6476=VECTOR ( 'NONE', #12144, 1000.000000000000000 ) ;
#6493=CARTESIAN_POINT ( 'NONE',  ( 0.05140428708382910328, -4.819072548984009607, -1.653121499799246719 ) ) ;
#6499=CONICAL_SURFACE ( 'NONE', #4716, 3.309499999999999886, 0.7853981633974407295 ) ;
#6535=CARTESIAN_POINT ( 'NONE',  ( -3.114822491369819039E-15, 4.452621892014636096, 2.287832656137190668 ) ) ;
#6552=CARTESIAN_POINT ( 'NONE',  ( 6.355827204229362870, 3.436818823786758070, 4.264647808192652434 ) ) ;
#6554=CARTESIAN_POINT ( 'NONE',  ( 0.000000000000000000, 0.000000000000000000, 0.000000000000000000 ) ) ;
#6560=CARTESIAN_POINT ( 'NONE',  ( 0.05140428708382505096, -3.841181488860373250, 3.346878500200758833 ) ) ;
#6586=VERTEX_POINT ( 'NONE', #7137 ) ;
#6587=PRODUCT_DEFINITION ( 'UNKNOWN', '', #3526, #12137 ) ;
#6603=CARTESIAN_POINT ( 'NONE',  ( 0.000000000000000000, 0.000000000000000000, 0.000000000000000000 ) ) ;
#6613=CARTESIAN_POINT ( 'NONE',  ( 6.371506350351446635, 5.409331239960136983, 0.8483282427581467777 ) ) ;
#6614=CARTESIAN_POINT ( 'NONE',  ( 6.506987859255521478, -5.850751062354593302, 2.176274696337492837E-17 ) ) ;
#6624=FACE_OUTER_BOUND ( 'NONE', #5982, .T. ) ;
#6627=CARTESIAN_POINT ( 'NONE',  ( 0.000000000000000000, 0.000000000000000000, 4.000000000000000000 ) ) ;
#6637=EDGE_CURVE ( 'NONE', #5736, #4363, #9331, .T. ) ;
#6646=LINE ( 'NONE', #3593, #1998 ) ;
#6672=CARTESIAN_POINT ( 'NONE',  ( 0.1739375980333722760, 3.358985280702821097, 4.182066831946702479 ) ) ;
#6683=CARTESIAN_POINT ( 'NONE',  ( 6.445127866599366762, 5.657054305385774917, 0.4229901806197435277 ) ) ;
#6684=DIRECTION ( 'NONE',  ( 0.000000000000000000, 0.000000000000000000, 1.000000000000000000 ) ) ;
#6695=CARTESIAN_POINT ( 'NONE',  ( 6.245824673232988289, 3.903127342724162840, 3.450227696316072734 ) ) ;
#6709=ORIENTED_EDGE ( 'NONE', *, *, #1511, .F. ) ;
#6732=DIRECTION ( 'NONE',  ( -1.000000000000000000, -0.000000000000000000, -0.000000000000000000 ) ) ;
#6739=EDGE_LOOP ( 'NONE', ( #6363, #9153, #4639, #11321, #2003 ) ) ;
#6740=DIRECTION ( 'NONE',  ( 0.000000000000000000, 0.000000000000000000, -1.000000000000000000 ) ) ;
#6755=DIRECTION ( 'NONE',  ( -1.000000000000000000, -0.000000000000000000, 0.000000000000000000 ) ) ;
#6760=CARTESIAN_POINT ( 'NONE',  ( 6.204460410672266946, 4.828986228461177532, 1.635950503255240607 ) ) ;
#6774=LINE ( 'NONE', #7748, #3995 ) ;
#6787=EDGE_CURVE ( 'NONE', #11251, #9307, #9972, .T. ) ;
#6790=CARTESIAN_POINT ( 'NONE',  ( 6.244889965166093404, 4.918546365148221078, -1.691415889817839302 ) ) ;
#6826=CARTESIAN_POINT ( 'NONE',  ( 6.390983168987730778, -3.014662706507984513, -5.000000000000000000 ) ) ;
#6850=ORIENTED_EDGE ( 'NONE', *, *, #7882, .T. ) ;
#6877=CARTESIAN_POINT ( 'NONE',  ( 8.500000000000000000, -2.886751345948119774, 4.999999999999999112 ) ) ;
#6882=EDGE_LOOP ( 'NONE', ( #5119, #5369, #7456, #473, #2786 ) ) ;
#6898=CARTESIAN_POINT ( 'NONE',  ( 0.1973348417602843741, -1.936114729415326696, -5.000000000000000000 ) ) ;
#6910=CARTESIAN_POINT ( 'NONE',  ( 6.367873360227558344, -2.886751345948133984, -5.000000000000000000 ) ) ;
#6916=CARTESIAN_POINT ( 'NONE',  ( 6.367873360227556567, 2.886751345948123770, -5.000000000000000000 ) ) ;
#6918=ORIENTED_EDGE ( 'NONE', *, *, #9413, .F. ) ;
#6938=VECTOR ( 'NONE', #9692, 999.9999999999998863 ) ;
#6948=CARTESIAN_POINT ( 'NONE',  ( 7.900000000000002132, 0.000000000000000000, 0.000000000000000000 ) ) ;
#6959=EDGE_CURVE ( 'NONE', #5390, #1735, #1547, .T. ) ;
#6961=ADVANCED_FACE ( 'NONE', ( #12076 ), #11733, .F. ) ;
#6982=CARTESIAN_POINT ( 'NONE',  ( 0.000000000000000000, 0.000000000000000000, 0.000000000000000000 ) ) ;
#6989=VECTOR ( 'NONE', #11086, 1000.000000000000000 ) ;
#6993=EDGE_CURVE ( 'NONE', #5480, #4363, #2929, .T. ) ;
#7006=ORIENTED_EDGE ( 'NONE', *, *, #1265, .T. ) ;
#7020=ORIENTED_EDGE ( 'NONE', *, *, #3988, .F. ) ;
#7029=DIRECTION ( 'NONE',  ( 0.000000000000000000, 0.000000000000000000, 1.000000000000000000 ) ) ;
#7092=FACE_BOUND ( 'NONE', #11726, .T. ) ;
#7099=CARTESIAN_POINT ( 'NONE',  ( 6.541334219041339715, -5.921300567812618709, 0.03049376373817737351 ) ) ;
#7103=CARTESIAN_POINT ( 'NONE',  ( 6.212060063025226064, 2.039954613758735658, -5.000000000000000000 ) ) ;
#7119=CARTESIAN_POINT ( 'NONE',  ( 0.4465819873852049926, -5.773502691896263528, -3.127607256515468906E-17 ) ) ;
#7121=CIRCLE ( 'NONE', #1351, 3.309499999999999886 ) ;
#7137=CARTESIAN_POINT ( 'NONE',  ( 6.244297270354683960, 1.802013835206515036E-11, 5.105276777067893512 ) ) ;
#7139=DIRECTION ( 'NONE',  ( 0.000000000000000000, 0.000000000000000000, -1.000000000000000000 ) ) ;
#7161=DIRECTION ( 'NONE',  ( -1.000000000000000000, -0.000000000000000000, -0.000000000000000000 ) ) ;
#7166=AXIS2_PLACEMENT_3D ( 'NONE', #9442, #13642, #9974 ) ;
#7170=ORIENTED_EDGE ( 'NONE', *, *, #8802, .T. ) ;
#7172=CARTESIAN_POINT ( 'NONE',  ( 6.357976367241631621, 3.426708043487392885, -4.282301071214502208 ) ) ;
#7190=EDGE_LOOP ( 'NONE', ( #8311, #1699, #2995, #1666, #3825 ) ) ;
#7217=AXIS2_PLACEMENT_3D ( 'NONE', #9635, #291, #2295 ) ;
#7219=ORIENTED_EDGE ( 'NONE', *, *, #3551, .T. ) ;
#7226=CARTESIAN_POINT ( 'NONE',  ( -3.574908632038010113E-15, 4.821944789745366222, -1.648146632869000427 ) ) ;
#7239=DIRECTION ( 'NONE',  ( 0.000000000000000000, 0.8660254037844375974, -0.5000000000000018874 ) ) ;
#7245=CARTESIAN_POINT ( 'NONE',  ( 6.420058897733096792, -2.891482565094587898, 5.008194711943423805 ) ) ;
#7263=CARTESIAN_POINT ( 'NONE',  ( 6.270568613849412998, -3.932080789230354867, 3.401571648088637101 ) ) ;
#7270=ORIENTED_EDGE ( 'NONE', *, *, #1265, .F. ) ;
#7289=VERTEX_POINT ( 'NONE', #2387 ) ;
#7296=EDGE_CURVE ( 'NONE', #11340, #3318, #9924, .T. ) ;
#7312=PLANE ( 'NONE',  #783 ) ;
#7316=CARTESIAN_POINT ( 'NONE',  ( 6.095473853218515536, 4.853892138986921623, -1.592812200815479695 ) ) ;
#7317=CARTESIAN_POINT ( 'NONE',  ( 6.541171370350062020, -2.986177670315871335, 5.112746295475706582 ) ) ;
#7332=EDGE_CURVE ( 'NONE', #10855, #9257, #2289, .T. ) ;
#7349=CARTESIAN_POINT ( 'NONE',  ( 6.506891779418575439, -5.826362946429633816, -0.09155664655282159947 ) ) ;
#7357=ADVANCED_FACE ( 'NONE', ( #852 ), #9715, .F. ) ;
#7370=CARTESIAN_POINT ( 'NONE',  ( 6.244297270353399654, -0.9889575675955545320, 5.105276777067856209 ) ) ;
#7393=ORIENTED_EDGE ( 'NONE', *, *, #6959, .T. ) ;
#7411=B_SPLINE_CURVE_WITH_KNOTS ( 'NONE', 3,
 ( #3411, #11838, #8535, #7698, #5365 ),
 .UNSPECIFIED., .F., .F.,
 ( 4, 1, 4 ),
 ( 0.000000000000000000, 0.002886751345948131153, 0.005773502691896262307 ),
 .UNSPECIFIED. ) ;
#7427=CARTESIAN_POINT ( 'NONE',  ( 6.495567275915088423, 2.917443832164887230, -5.053160945538039961 ) ) ;
#7453=CARTESIAN_POINT ( 'NONE',  ( 6.452281807715811723, -5.797857616945994330, 1.289641217033754180E-15 ) ) ;
#7456=ORIENTED_EDGE ( 'NONE', *, *, #6449, .T. ) ;
#7464=DIRECTION ( 'NONE',  ( -0.000000000000000000, 0.000000000000000000, 1.000000000000000000 ) ) ;
#7501=DIRECTION ( 'NONE',  ( 0.000000000000000000, -0.5000000000000001110, 0.8660254037844387076 ) ) ;
#7502=ORIENTED_EDGE ( 'NONE', *, *, #7296, .T. ) ;
#7557=ADVANCED_FACE ( 'NONE', ( #10480 ), #1664, .F. ) ;
#7566=CARTESIAN_POINT ( 'NONE',  ( 0.05140428708382657752, 4.819072548984005167, 1.653121499799249605 ) ) ;
#7572=CARTESIAN_POINT ( 'NONE',  ( 6.385552186430388133, 2.886751345948125991, 4.999999999999999112 ) ) ;
#7584=CARTESIAN_POINT ( 'NONE',  ( 6.495567275915080430, -5.834887664329776236, 2.176274696337492837E-17 ) ) ;
#7593=EDGE_LOOP ( 'NONE', ( #11464, #3605, #4011, #11812 ) ) ;
#7595=CARTESIAN_POINT ( 'NONE',  ( -4.113721387458914807E-15, -4.207632145829740544, 2.712167343862823099 ) ) ;
#7620=ORIENTED_EDGE ( 'NONE', *, *, #9564, .T. ) ;
#7622=CIRCLE ( 'NONE', #5632, 4.999999999999999112 ) ;
#7642=DIRECTION ( 'NONE',  ( -1.000000000000000000, -0.000000000000000000, -0.000000000000000000 ) ) ;
#7643=CARTESIAN_POINT ( 'NONE',  ( 0.4465819873852049926, -5.773502691896263528, -3.127607256515468906E-17 ) ) ;
#7648=EDGE_CURVE ( 'NONE', #9438, #11355, #3791, .T. ) ;
#7656=VERTEX_POINT ( 'NONE', #10323 ) ;
#7670=DIRECTION ( 'NONE',  ( -1.000000000000000000, -0.000000000000000000, -0.000000000000000000 ) ) ;
#7684=ADVANCED_FACE ( 'NONE', ( #9086 ), #5910, .F. ) ;
#7698=CARTESIAN_POINT ( 'NONE',  ( 6.196878017913831194, 3.367876570272813730, -4.166666666666668739 ) ) ;
#7702=EDGE_LOOP ( 'NONE', ( #6330, #8205, #10087, #6709, #6189 ) ) ;
#7720=CARTESIAN_POINT ( 'NONE',  ( 6.367873360227559232, -5.773502691896263528, 0.000000000000000000 ) ) ;
#7726=CARTESIAN_POINT ( 'NONE',  ( 8.500000000000000000, 2.886751345948125991, 4.999999999999999112 ) ) ;
#7732=CARTESIAN_POINT ( 'NONE',  ( 6.212068001622437663, 3.310128279683251851, 4.266689640018040741 ) ) ;
#7748=CARTESIAN_POINT ( 'NONE',  ( 8.500000000000000000, -2.886751345948133984, -5.000000000000000000 ) ) ;
#7770=CARTESIAN_POINT ( 'NONE',  ( 7.336184427528458230, 9.926022037524705097E-16, 8.105212085995399107 ) ) ;
#7771=CIRCLE ( 'NONE', #9534, 7.900000000000002132 ) ;
#7786=CARTESIAN_POINT ( 'NONE',  ( 6.534838248920897819, 2.951765777552412651, 5.112608298763836601 ) ) ;
#7796=EDGE_LOOP ( 'NONE', ( #9084, #12438, #12404, #2083, #1700, #9133 ) ) ;
#7824=ORIENTED_EDGE ( 'NONE', *, *, #6449, .F. ) ;
#7825=EDGE_LOOP ( 'NONE', ( #10217, #3827, #1859, #6918 ) ) ;
#7847=DIRECTION ( 'NONE',  ( 1.000000000000000000, 0.000000000000000000, 0.000000000000000000 ) ) ;
#7864=CARTESIAN_POINT ( 'NONE',  ( 6.367873360227555679, -2.886751345948119774, 4.999999999999999112 ) ) ;
#7867=CARTESIAN_POINT ( 'NONE',  ( 53.50000000000000000, 0.000000000000000000, 0.000000000000000000 ) ) ;
#7870=CARTESIAN_POINT ( 'NONE',  ( 6.207660606243411650, -2.016205878028328957, -5.000000000000000000 ) ) ;
#7882=EDGE_CURVE ( 'NONE', #6095, #4029, #1594, .T. ) ;
#7900=FACE_OUTER_BOUND ( 'NONE', #2037, .T. ) ;
#7942=( GEOMETRIC_REPRESENTATION_CONTEXT ( 3 ) GLOBAL_UNCERTAINTY_ASSIGNED_CONTEXT ( ( #5791 ) ) GLOBAL_UNIT_ASSIGNED_CONTEXT ( ( #4751, #10057, #1477 ) ) REPRESENTATION_CONTEXT ( 'NONE', 'WORKASPACE' ) );
#7944=CONICAL_SURFACE ( 'NONE', #1296, 5.000000000000000000, 1.047197551196600296 ) ;
#7947=CARTESIAN_POINT ( 'NONE',  ( 6.466260427357664042, -2.904280683598015500, -5.030361703432624232 ) ) ;
#7998=CARTESIAN_POINT ( 'NONE',  ( 6.357976367241527704, -5.421935536068480666, -0.8264656814046078548 ) ) ;
#8000=CARTESIAN_POINT ( 'NONE',  ( 6.541334219041338827, 5.921300567812616933, -0.03049376373817709943 ) ) ;
#8010=ORIENTED_EDGE ( 'NONE', *, *, #4647, .F. ) ;
#8016=CARTESIAN_POINT ( 'NONE',  ( 6.534224484704326485, -2.950930484791631780, -5.111161529262894909 ) ) ;
#8033=CARTESIAN_POINT ( 'NONE',  ( 0.000000000000000000, 0.000000000000000000, 5.000000000000000000 ) ) ;
#8069=CARTESIAN_POINT ( 'NONE',  ( 6.207530437345012864, 4.849805425595251407, -1.599890596046337210 ) ) ;
#8089=CARTESIAN_POINT ( 'NONE',  ( 6.518095160331714766, -2.933089652807550074, -5.080260301817226321 ) ) ;
#8113=B_SPLINE_CURVE_WITH_KNOTS ( 'NONE', 3,
 ( #1948, #6193, #9489, #2148, #10458, #8525, #11572, #7427, #10662, #1173, #972, #5224, #901, #12726, #6396, #10594 ),
 .UNSPECIFIED., .F., .F.,
 ( 4, 3, 3, 3, 3, 4 ),
 ( -2.669610558406242719E-06, 0.000000000000000000, 5.703179328865551904E-05, 0.0001157653700805886653, 0.0001686517580799675017, 0.0002219032271235110720 ),
 .UNSPECIFIED. ) ;
#8131=VERTEX_POINT ( 'NONE', #8866 ) ;
#8138=CARTESIAN_POINT ( 'NONE',  ( 6.095473853218072335, -3.806361898857768544, -3.407187799184005161 ) ) ;
#8140=CARTESIAN_POINT ( 'NONE',  ( 53.50000000000000000, 0.000000000000000000, 0.000000000000000000 ) ) ;
#8141=FACE_OUTER_BOUND ( 'NONE', #7702, .T. ) ;
#8148=EDGE_CURVE ( 'NONE', #5736, #7289, #13649, .T. ) ;
#8156=CONICAL_SURFACE ( 'NONE', #2619, 5.000000000000000000, 1.047197551196600296 ) ;
#8167=ORIENTED_EDGE ( 'NONE', *, *, #6440, .T. ) ;
#8174=CARTESIAN_POINT ( 'NONE',  ( 6.534838248920896930, -2.951765777552406878, 5.112608298763836601 ) ) ;
#8189=CARTESIAN_POINT ( 'NONE',  ( 0.08165819712376902462, 3.720292241887087403, -3.556264818047239817 ) ) ;
#8205=ORIENTED_EDGE ( 'NONE', *, *, #3551, .F. ) ;
#8207=CARTESIAN_POINT ( 'NONE',  ( 6.212068001623052282, 5.350125758160769962, -0.7333103599825900876 ) ) ;
#8240=CONICAL_SURFACE ( 'NONE', #5812, 5.000000000000000000, 1.047197551196600296 ) ;
#8255=ADVANCED_FACE ( 'NONE', ( #10788 ), #2889, .T. ) ;
#8264=B_SPLINE_CURVE_WITH_KNOTS ( 'NONE', 3,
 ( #773, #12331, #2799, #3695, #13358, #11297 ),
 .UNSPECIFIED., .F., .F.,
 ( 4, 2, 4 ),
 ( 0.000000000000000000, 0.001488912493401906576, 0.002977824986803813152 ),
 .UNSPECIFIED. ) ;
#8276=AXIS2_PLACEMENT_3D ( 'NONE', #12334, #4742, #8958 ) ;
#8280=CARTESIAN_POINT ( 'NONE',  ( 6.403457969954084561, -2.888443235695444145, 5.002930439003169028 ) ) ;
#8281=SURFACE_STYLE_USAGE ( .BOTH. , #1904 ) ;
#8294=CARTESIAN_POINT ( 'NONE',  ( 0.000000000000000000, 0.000000000000000000, 0.000000000000000000 ) ) ;
#8311=ORIENTED_EDGE ( 'NONE', *, *, #6959, .F. ) ;
#8314=CARTESIAN_POINT ( 'NONE',  ( 6.507056315241511513, -2.833450876375909644, 5.092319121366346124 ) ) ;
#8324=VERTEX_POINT ( 'NONE', #748 ) ;
#8332=CARTESIAN_POINT ( 'NONE',  ( 0.1996310553826630974, 1.947030205581109730, -5.000000000000000888 ) ) ;
#8342=DIRECTION ( 'NONE',  ( -0.000000000000000000, 0.000000000000000000, -1.000000000000000000 ) ) ;
#8346=VERTEX_POINT ( 'NONE', #13265 ) ;
#8349=CARTESIAN_POINT ( 'NONE',  ( 6.506891779418572774, 5.826362946429627598, 0.09155664655281574305 ) ) ;
#8372=VERTEX_POINT ( 'NONE', #12176 ) ;
#8374=AXIS2_PLACEMENT_3D ( 'NONE', #3420, #9135, #6740 ) ;
#8377=DIRECTION ( 'NONE',  ( 0.000000000000000000, -1.224646799147353700E-16, 1.000000000000000000 ) ) ;
#8378=CARTESIAN_POINT ( 'NONE',  ( 6.323279575526007612, -3.325091652217148308, 4.240772318536393470 ) ) ;
#8395=CARTESIAN_POINT ( 'NONE',  ( 0.000000000000000000, 0.000000000000000000, -5.000000000000000000 ) ) ;
#8413=CARTESIAN_POINT ( 'NONE',  ( 6.518095160331712989, 2.933089652807542524, 5.080260301817225432 ) ) ;
#8466=CARTESIAN_POINT ( 'NONE',  ( 52.80949999999998568, 0.000000000000000000, 0.000000000000000000 ) ) ;
#8478=ADVANCED_FACE ( 'NONE', ( #6320 ), #2477, .F. ) ;
#8494=EDGE_CURVE ( 'NONE', #12356, #8346, #12508, .T. ) ;
#8525=CARTESIAN_POINT ( 'NONE',  ( 6.518095160331718319, 2.933089652807546077, -5.080260301817233426 ) ) ;
#8535=CARTESIAN_POINT ( 'NONE',  ( 5.991014884144048480, 4.330127018922193649, -2.499999999999998668 ) ) ;
#8544=CARTESIAN_POINT ( 'NONE',  ( 53.50000000000000000, 4.475777889183788807E-16, -3.309499999999999886 ) ) ;
#8567=( NAMED_UNIT ( * ) SI_UNIT ( $, .STERADIAN. ) SOLID_ANGLE_UNIT ( ) );
#8574=CARTESIAN_POINT ( 'NONE',  ( 8.500000000000000000, 0.000000000000000000, 7.900000000000002132 ) ) ;
#8591=CARTESIAN_POINT ( 'NONE',  ( 0.3117969352650132309, 2.419842229202153305, -4.999999999999999112 ) ) ;
#8596=CIRCLE ( 'NONE', #9472, 4.000000000000000000 ) ;
#8633=EDGE_CURVE ( 'NONE', #7656, #9307, #6646, .T. ) ;
#8638=EDGE_CURVE ( 'NONE', #844, #11042, #6774, .T. ) ;
#8671=LINE ( 'NONE', #7770, #6457 ) ;
#8682=CARTESIAN_POINT ( 'NONE',  ( 6.507056549636238252, 2.993353539201078828, 4.999999999999999112 ) ) ;
#8689=CARTESIAN_POINT ( 'NONE',  ( 8.500000000000000000, 0.000000000000000000, 0.000000000000000000 ) ) ;
#8709=AXIS2_PLACEMENT_3D ( 'NONE', #13284, #6126, #13560 ) ;
#8710=ORIENTED_EDGE ( 'NONE', *, *, #12099, .T. ) ;
#8755=CARTESIAN_POINT ( 'NONE',  ( 6.385552186430389909, -5.773502691896263528, -1.564818079814629131E-31 ) ) ;
#8802=EDGE_CURVE ( 'NONE', #844, #5390, #2099, .T. ) ;
#8811=CARTESIAN_POINT ( 'NONE',  ( 6.357987042335720318, 1.995285544161303992, 5.108766985362874102 ) ) ;
#8820=CARTESIAN_POINT ( 'NONE',  ( 7.336184427528458230, 9.926022037524705097E-16, 8.105212085995399107 ) ) ;
#8827=UNCERTAINTY_MEASURE_WITH_UNIT (LENGTH_MEASURE( 1.000000000000000082E-05 ), #63, 'distance_accuracy_value', 'NONE');
#8862=ORIENTED_EDGE ( 'NONE', *, *, #2788, .T. ) ;
#8863=CARTESIAN_POINT ( 'NONE',  ( 6.244004651191001898, 4.178905357954649347, -2.972460101650454156 ) ) ;
#8866=CARTESIAN_POINT ( 'NONE',  ( 6.534838248920897819, 2.951765777552412651, 5.112608298763836601 ) ) ;
#8870=B_SPLINE_CURVE_WITH_KNOTS ( 'NONE', 3,
 ( #1509, #3607, #2559, #4645, #8863, #6790, #5756, #9957 ),
 .UNSPECIFIED., .F., .F.,
 ( 4, 2, 2, 4 ),
 ( 0.000000000000000000, 0.001493104274552340587, 0.002986208549104681607, 0.005972417098209364950 ),
 .UNSPECIFIED. ) ;
#8877=EDGE_LOOP ( 'NONE', ( #10983, #9659, #4644, #1119 ) ) ;
#8879=ADVANCED_FACE ( 'NONE', ( #3795 ), #9742, .T. ) ;
#8883=FACE_OUTER_BOUND ( 'NONE', #12952, .T. ) ;
#8902=PLANE ( 'NONE',  #3719 ) ;
#8909=CARTESIAN_POINT ( 'NONE',  ( 6.245813541929285506, 1.036329910265332499, -5.105320956836708390 ) ) ;
#8914=EDGE_CURVE ( 'NONE', #8346, #844, #11335, .T. ) ;
#8920=B_SPLINE_CURVE_WITH_KNOTS ( 'NONE', 3,
 ( #13020, #6683, #6613, #2584, #10690, #5451, #6552, #7786 ),
 .UNSPECIFIED., .F., .F.,
 ( 4, 2, 2, 4 ),
 ( 0.000000000000000000, 0.001493104274552339720, 0.002986208549104679439, 0.005972417098209361480 ),
 .UNSPECIFIED. ) ;
#8958=DIRECTION ( 'NONE',  ( 0.000000000000000000, 0.000000000000000000, 1.000000000000000000 ) ) ;
#8966=CARTESIAN_POINT ( 'NONE',  ( 6.541171661047875396, 2.934678558896536504, 5.142480235691129664 ) ) ;
#8975=ORIENTED_EDGE ( 'NONE', *, *, #3811, .T. ) ;
#8980=CARTESIAN_POINT ( 'NONE',  ( 6.534533895392296010, -2.951347675328743314, -5.111884124469654900 ) ) ;
#8986=ADVANCED_FACE ( 'NONE', ( #12638 ), #9261, .F. ) ;
#8988=CARTESIAN_POINT ( 'NONE',  ( 6.196878017913833858, -1.924500897298759172, -5.000000000000000888 ) ) ;
#9032=CARTESIAN_POINT ( 'NONE',  ( 0.000000000000000000, 0.000000000000000000, 0.000000000000000000 ) ) ;
#9036=CARTESIAN_POINT ( 'NONE',  ( 6.092460485788117275, -1.005982284679170391, -5.000000000000000000 ) ) ;
#9084=ORIENTED_EDGE ( 'NONE', *, *, #13028, .F. ) ;
#9086=FACE_OUTER_BOUND ( 'NONE', #6882, .T. ) ;
#9102=CARTESIAN_POINT ( 'NONE',  ( 8.500000000000000000, 9.800365875394399578E-16, -7.900000000000002132 ) ) ;
#9103=CARTESIAN_POINT ( 'NONE',  ( 6.245824673233021151, 4.939548505212935758, -1.655093584846096366 ) ) ;
#9104=CARTESIAN_POINT ( 'NONE',  ( 6.242800618755285136, -4.918813924287352535, -1.690830708135802052 ) ) ;
#9109=CARTESIAN_POINT ( 'NONE',  ( 1.753358200816401209E-16, -0.4883827417527520920, -4.999999999999999112 ) ) ;
#9120=CARTESIAN_POINT ( 'NONE',  ( 6.371919382990606451, -1.972754410575515704, -5.108792907957607099 ) ) ;
#9133=ORIENTED_EDGE ( 'NONE', *, *, #6993, .F. ) ;
#9135=DIRECTION ( 'NONE',  ( 1.000000000000000000, 0.000000000000000000, 0.000000000000000000 ) ) ;
#9140=CARTESIAN_POINT ( 'NONE',  ( 7.336184427528458230, 0.000000000000000000, 0.000000000000000000 ) ) ;
#9153=ORIENTED_EDGE ( 'NONE', *, *, #9413, .T. ) ;
#9176=CARTESIAN_POINT ( 'NONE',  ( 6.527192678185834929, -2.941622124011297412, 5.095038975455882913 ) ) ;
#9191=CARTESIAN_POINT ( 'NONE',  ( 0.000000000000000000, 0.000000000000000000, 0.000000000000000000 ) ) ;
#9196=SHAPE_REPRESENTATION ( 'hex flange bolt small_iso_ISO 4162 - M8 x 45 x 22-N', ( #430 ), #7942 ) ;
#9199=CARTESIAN_POINT ( 'NONE',  ( 0.4465819873851989974, -2.886751345948120218, 4.999999999999999112 ) ) ;
#9218=ORIENTED_EDGE ( 'NONE', *, *, #6637, .F. ) ;
#9223=DIRECTION ( 'NONE',  ( 0.000000000000000000, -0.5000000000000011102, -0.8660254037844380415 ) ) ;
#9242=CARTESIAN_POINT ( 'NONE',  ( 6.323279575527231522, 3.325091652218045368, -4.240772318537636920 ) ) ;
#9257=VERTEX_POINT ( 'NONE', #12913 ) ;
#9261=PLANE ( 'NONE',  #5971 ) ;
#9269=STYLED_ITEM ( 'NONE', ( #853 ), #870 ) ;
#9276=CARTESIAN_POINT ( 'NONE',  ( 0.000000000000000000, 0.000000000000000000, 0.000000000000000000 ) ) ;
#9292=FACE_OUTER_BOUND ( 'NONE', #11794, .T. ) ;
#9300=CARTESIAN_POINT ( 'NONE',  ( 8.500000000000000000, 2.886751345948123770, -5.000000000000000000 ) ) ;
#9307=VERTEX_POINT ( 'NONE', #1851 ) ;
#9312=CARTESIAN_POINT ( 'NONE',  ( 6.495567275915087535, -2.917443832164882345, 5.053160945538040849 ) ) ;
#9314=ADVANCED_FACE ( 'NONE', ( #1782 ), #7944, .T. ) ;
#9331=CIRCLE ( 'NONE', #13283, 5.000000000000000000 ) ;
#9348=CARTESIAN_POINT ( 'NONE',  ( 6.445127866599367650, -5.657054305385780246, -0.4229901806197432501 ) ) ;
#9375=ORIENTED_EDGE ( 'NONE', *, *, #13349, .T. ) ;
#9381=CARTESIAN_POINT ( 'NONE',  ( 6.242800618755075526, 3.923709308887314950, -3.414402460853798171 ) ) ;
#9383=CARTESIAN_POINT ( 'NONE',  ( 6.323279575528418128, -5.335162385627848280, -0.7592276814619393077 ) ) ;
#9384=( LENGTH_UNIT ( ) NAMED_UNIT ( * ) SI_UNIT ( .MILLI., .METRE. ) );
#9393=CARTESIAN_POINT ( 'NONE',  ( 6.367873360227556567, 2.886751345948125991, 4.999999999999999112 ) ) ;
#9395=ORIENTED_EDGE ( 'NONE', *, *, #6073, .T. ) ;
#9404=CARTESIAN_POINT ( 'NONE',  ( 6.244004651191001010, -4.178905357954647570, 2.972460101650454600 ) ) ;
#9413=EDGE_CURVE ( 'NONE', #5998, #12021, #195, .T. ) ;
#9415=CARTESIAN_POINT ( 'NONE',  ( 6.355324643801638196, 1.972141403783284730, -5.108685331087993831 ) ) ;
#9426=CARTESIAN_POINT ( 'NONE',  ( 6.534224484704327374, 5.901860969583204941, 2.029550679094937724E-14 ) ) ;
#9438=VERTEX_POINT ( 'NONE', #10294 ) ;
#9439=FACE_OUTER_BOUND ( 'NONE', #11023, .T. ) ;
#9441=CARTESIAN_POINT ( 'NONE',  ( 6.403457969954081008, 2.888443235695449030, 5.002930439003169028 ) ) ;
#9442=CARTESIAN_POINT ( 'NONE',  ( 0.000000000000000000, 0.000000000000000000, 0.000000000000000000 ) ) ;
#9444=CARTESIAN_POINT ( 'NONE',  ( 6.362382503762741948, -2.018850626433581041, 5.108861885121540602 ) ) ;
#9472=AXIS2_PLACEMENT_3D ( 'NONE', #1820, #13290, #6066 ) ;
#9488=CARTESIAN_POINT ( 'NONE',  ( 6.420058897733093239, 5.782965130189194447, -1.451745169709246731E-16 ) ) ;
#9489=CARTESIAN_POINT ( 'NONE',  ( 6.534224484704323821, 2.950930484791612685, -5.111161529262899350 ) ) ;
#9500=DIRECTION ( 'NONE',  ( -1.000000000000000000, -0.000000000000000000, -0.000000000000000000 ) ) ;
#9510=CARTESIAN_POINT ( 'NONE',  ( 6.367873360227556567, 2.886751345948125991, 4.999999999999999112 ) ) ;
#9534=AXIS2_PLACEMENT_3D ( 'NONE', #11672, #7670, #11874 ) ;
#9551=CARTESIAN_POINT ( 'NONE',  ( 8.500000000000000000, 5.773502691896261751, 0.000000000000000000 ) ) ;
#9557=CARTESIAN_POINT ( 'NONE',  ( 6.527192678185836705, 5.883244248022287515, -9.347031149521713219E-14 ) ) ;
#9564=EDGE_CURVE ( 'NONE', #9257, #12356, #10262, .T. ) ;
#9573=CARTESIAN_POINT ( 'NONE',  ( 8.500000000000000000, -2.886751345948133984, -5.000000000000000000 ) ) ;
#9577=CARTESIAN_POINT ( 'NONE',  ( 6.533910050139694725, 2.950514251728050485, 5.110440592449069896 ) ) ;
#9585=FACE_OUTER_BOUND ( 'NONE', #1355, .T. ) ;
#9613=CARTESIAN_POINT ( 'NONE',  ( 6.534838248920900483, -5.903531555104836848, 4.671345613696493211E-16 ) ) ;
#9618=DIRECTION ( 'NONE',  ( 0.000000000000000000, -0.8660254037844380415, -0.5000000000000009992 ) ) ;
#9635=CARTESIAN_POINT ( 'NONE',  ( 7.900000000000002132, 0.000000000000000000, 7.900000000000002132 ) ) ;
#9652=CARTESIAN_POINT ( 'NONE',  ( 6.534224484704327374, -5.901860969583205829, 2.643887195172161483E-14 ) ) ;
#9659=ORIENTED_EDGE ( 'NONE', *, *, #2861, .F. ) ;
#9672=B_SPLINE_CURVE_WITH_KNOTS ( 'NONE', 3,
 ( #3229, #5248, #2046, #4132, #43 ),
 .UNSPECIFIED., .F., .F.,
 ( 4, 1, 4 ),
 ( 9.359404341228126911E-20, 0.002886751345948132021, 0.005773502691896264041 ),
 .UNSPECIFIED. ) ;
#9692=DIRECTION ( 'NONE',  ( -0.7071067811865530128, 0.000000000000000000, 0.7071067811865421326 ) ) ;
#9693=CARTESIAN_POINT ( 'NONE',  ( 7.900000000000002132, 0.000000000000000000, 0.000000000000000000 ) ) ;
#9713=CARTESIAN_POINT ( 'NONE',  ( 6.323290364500451233, 2.010128762267162639, 4.999999999999998224 ) ) ;
#9715=( BOUNDED_SURFACE ( )  B_SPLINE_SURFACE ( 3, 2, ( 
 ( #2810, #5928, #13368 ),
 ( #2876, #637, #926 ),
 ( #8138, #5176, #1685 ),
 ( #12484, #4889, #9104 ),
 ( #4963, #9383, #7998 ),
 ( #3775, #12412, #7099 ) ),
 .UNSPECIFIED., .F., .F., .F. ) 
 B_SPLINE_SURFACE_WITH_KNOTS ( ( 4, 2, 4 ),
 ( 3, 3 ),
 ( 0.02367865728600892020, 0.02663179453327098323, 0.02958493178053304279 ),
 ( 0.000000000000000000, 1.000000000000000000 ),
 .UNSPECIFIED. ) 
 GEOMETRIC_REPRESENTATION_ITEM ( )  RATIONAL_B_SPLINE_SURFACE ( (
 ( 1.000000000000000000, 0.8047781103519402457, 1.000000000000000000),
 ( 1.000000000000000000, 0.8123785825973208752, 1.000000000000000000),
 ( 1.000000000000000000, 0.8190671539297160741, 1.000000000000000000),
 ( 1.000000000000000000, 0.8192352255325974220, 1.000000000000000000),
 ( 1.000000000000000000, 0.8126129676842754890, 1.000000000000000000),
 ( 1.000000000000000000, 0.8047712537969723412, 1.000000000000000000) ) ) 
 REPRESENTATION_ITEM ( '' )  SURFACE ( )  );
#9724=CARTESIAN_POINT ( 'NONE',  ( 0.1983443223721600701, -5.300482436767282479, -0.8192951148925879945 ) ) ;
#9738=EDGE_CURVE ( 'NONE', #4029, #11042, #10578, .T. ) ;
#9742=CONICAL_SURFACE ( 'NONE', #1079, 5.000000000000000000, 1.047197551196600296 ) ;
#9746=DIRECTION ( 'NONE',  ( 0.000000000000000000, 0.000000000000000000, -1.000000000000000000 ) ) ;
#9770=CARTESIAN_POINT ( 'NONE',  ( 0.4465819873852039379, 5.773502691896261751, 3.331019006688249527E-17 ) ) ;
#9787=CARTESIAN_POINT ( 'NONE',  ( 6.403457969954083673, -5.776886471390910494, 4.740078563816561288E-16 ) ) ;
#9789=CARTESIAN_POINT ( 'NONE',  ( 0.01055556052339245120, -4.575665857285984295, -2.074714256722479888 ) ) ;
#9797=CARTESIAN_POINT ( 'NONE',  ( 0.4465819873851989974, -2.886751345948120218, 4.999999999999999112 ) ) ;
#9832=CARTESIAN_POINT ( 'NONE',  ( 0.3117969352650131198, 2.419842229202155970, 4.999999999999999112 ) ) ;
#9844=DIRECTION ( 'NONE',  ( 1.000000000000000000, 0.000000000000000000, 0.000000000000000000 ) ) ;
#9881=ADVANCED_FACE ( 'NONE', ( #8141 ), #4876, .F. ) ;
#9902=AXIS2_PLACEMENT_3D ( 'NONE', #5578, #2445, #6684 ) ;
#9924=LINE ( 'NONE', #6627, #3341 ) ;
#9941=CARTESIAN_POINT ( 'NONE',  ( 6.244297270355322560, -0.4917101305082151597, -5.105276777067913052 ) ) ;
#9957=CARTESIAN_POINT ( 'NONE',  ( 6.534838248920899595, 5.903531555104835071, 8.098083288904839678E-18 ) ) ;
#9967=CYLINDRICAL_SURFACE ( 'NONE', #10212, 4.000000000000000000 ) ;
#9971=VERTEX_POINT ( 'NONE', #2044 ) ;
#9972=CIRCLE ( 'NONE', #10206, 0.5999999999999980904 ) ;
#9974=DIRECTION ( 'NONE',  ( 0.000000000000000000, 0.000000000000000000, -1.000000000000000000 ) ) ;
#9992=CARTESIAN_POINT ( 'NONE',  ( 6.390983399715593372, 5.837459000499768180, -0.1107755759658281131 ) ) ;
#10015=CARTESIAN_POINT ( 'NONE',  ( 6.196878017913830305, 1.924500897298746960, -4.999999999999999112 ) ) ;
#10022=ADVANCED_FACE ( 'NONE', ( #9585 ), #1326, .T. ) ;
#10039=ORIENTED_EDGE ( 'NONE', *, *, #12932, .T. ) ;
#10053=ORIENTED_EDGE ( 'NONE', *, *, #6993, .T. ) ;
#10057=( NAMED_UNIT ( * ) PLANE_ANGLE_UNIT ( ) SI_UNIT ( $, .RADIAN. ) );
#10058=CARTESIAN_POINT ( 'NONE',  ( 6.390820841722129941, 2.823237767533145703, 5.110008744785254464 ) ) ;
#10062=CARTESIAN_POINT ( 'NONE',  ( 0.04201760816084261496, -0.9730571234389092661, -5.000000000000000888 ) ) ;
#10074=LINE ( 'NONE', #4696, #5939 ) ;
#10080=CARTESIAN_POINT ( 'NONE',  ( 6.196878017913830305, 3.367876570272813730, 4.166666666666666075 ) ) ;
#10087=ORIENTED_EDGE ( 'NONE', *, *, #10150, .F. ) ;
#10093=DIRECTION ( 'NONE',  ( -1.000000000000000000, -0.000000000000000000, -0.000000000000000000 ) ) ;
#10124=VERTEX_POINT ( 'NONE', #5353 ) ;
#10126=MECHANICAL_DESIGN_GEOMETRIC_PRESENTATION_REPRESENTATION('',(#11294),#1056);
#10128=CARTESIAN_POINT ( 'NONE',  ( 6.534224484704323821, -2.950930484791555841, 5.111161529262928660 ) ) ;
#10130=DIRECTION ( 'NONE',  ( -1.000000000000000000, -0.000000000000000000, -0.000000000000000000 ) ) ;
#10135=CARTESIAN_POINT ( 'NONE',  ( 0.4465819873849485311, -2.886751345948517677, -5.000000000000000000 ) ) ;
#10148=ADVANCED_FACE ( 'NONE', ( #6332 ), #4106, .F. ) ;
#10150=EDGE_CURVE ( 'NONE', #12408, #6051, #8113, .T. ) ;
#10153=DIRECTION ( 'NONE',  ( 0.000000000000000000, 0.000000000000000000, -1.000000000000000000 ) ) ;
#10206=AXIS2_PLACEMENT_3D ( 'NONE', #4153, #10577, #8377 ) ;
#10212=AXIS2_PLACEMENT_3D ( 'NONE', #1731, #484, #10936 ) ;
#10213=EDGE_CURVE ( 'NONE', #11355, #486, #2351, .T. ) ;
#10217=ORIENTED_EDGE ( 'NONE', *, *, #11276, .T. ) ;
#10218=FACE_OUTER_BOUND ( 'NONE', #12856, .T. ) ;
#10221=DIRECTION ( 'NONE',  ( -1.000000000000000000, -0.000000000000000000, -0.000000000000000000 ) ) ;
#10230=ORIENTED_EDGE ( 'NONE', *, *, #3988, .T. ) ;
#10262=B_SPLINE_CURVE_WITH_KNOTS ( 'NONE', 3,
 ( #8174, #12502, #10366, #7263, #9404, #10501, #13600, #4144 ),
 .UNSPECIFIED., .F., .F.,
 ( 4, 2, 2, 4 ),
 ( 0.000000000000000000, 0.001493104274552342322, 0.002986208549104684210, 0.005972417098209366684 ),
 .UNSPECIFIED. ) ;
#10294=CARTESIAN_POINT ( 'NONE',  ( 53.50000000000000000, 0.000000000000000000, 3.309499999999999886 ) ) ;
#10315=ORIENTED_EDGE ( 'NONE', *, *, #8914, .F. ) ;
#10323=CARTESIAN_POINT ( 'NONE',  ( 6.244297270354684848, -1.798312406574552930E-11, -5.105276777067894400 ) ) ;
#10366=CARTESIAN_POINT ( 'NONE',  ( 6.371506350351443082, -3.439339428956426747, 4.260454149911180544 ) ) ;
#10411=CARTESIAN_POINT ( 'NONE',  ( 6.518095160331717430, -2.933089652807539416, 5.080260301817235202 ) ) ;
#10447=CARTESIAN_POINT ( 'NONE',  ( 6.244297270353404095, 0.9889575675955796230, -5.105276777067857097 ) ) ;
#10458=CARTESIAN_POINT ( 'NONE',  ( 6.527192678185834929, 2.941622124011056272, -5.095038975456026797 ) ) ;
#10477=CARTESIAN_POINT ( 'NONE',  ( 6.436591462021355348, 2.894509378375960118, 5.013437306331775645 ) ) ;
#10480=FACE_OUTER_BOUND ( 'NONE', #4302, .T. ) ;
#10501=CARTESIAN_POINT ( 'NONE',  ( 6.244889965166096957, -4.918546365148221078, 1.691415889817839746 ) ) ;
#10511=CARTESIAN_POINT ( 'NONE',  ( 6.327632967270674591, -5.346704644969953790, 0.7392359018479527366 ) ) ;
#10525=CARTESIAN_POINT ( 'NONE',  ( 6.403457969954082785, 5.776886471390908717, -1.402224347649779865E-18 ) ) ;
#10555=ORIENTED_EDGE ( 'NONE', *, *, #9738, .T. ) ;
#10570=EDGE_CURVE ( 'NONE', #486, #8372, #10074, .T. ) ;
#10574=CONICAL_SURFACE ( 'NONE', #8374, 8.105212085995399107, 1.221730476396037490 ) ;
#10577=DIRECTION ( 'NONE',  ( -0.000000000000000000, 1.000000000000000000, 1.224646799147353207E-16 ) ) ;
#10578=B_SPLINE_CURVE_WITH_KNOTS ( 'NONE', 3,
 ( #5524, #9109, #10062, #6898, #13372, #10135 ),
 .UNSPECIFIED., .F., .F.,
 ( 4, 2, 4 ),
 ( 0.01799235506992015107, 0.01945319861728521740, 0.02091404216465028373 ),
 .UNSPECIFIED. ) ;
#10579=CARTESIAN_POINT ( 'NONE',  ( 6.244004651191001010, -4.663678638742299931, -2.132808149174403312 ) ) ;
#10594=CARTESIAN_POINT ( 'NONE',  ( 6.367873360227556567, 2.886751345948123770, -5.000000000000000000 ) ) ;
#10612=CARTESIAN_POINT ( 'NONE',  ( 6.420058897733091463, 2.891482565094592339, 5.008194711943422028 ) ) ;
#10657=EDGE_LOOP ( 'NONE', ( #11969, #459, #10555 ) ) ;
#10662=CARTESIAN_POINT ( 'NONE',  ( 6.481779955677444249, 2.910222513313288850, -5.040653254389421356 ) ) ;
#10680=EDGE_LOOP ( 'NONE', ( #10971, #4101, #9218 ) ) ;
#10690=CARTESIAN_POINT ( 'NONE',  ( 6.244004651191001010, 4.663678638742294602, 2.132808149174402867 ) ) ;
#10725=ADVANCED_FACE ( 'NONE', ( #10218 ), #2167, .T. ) ;
#10755=DIRECTION ( 'NONE',  ( 1.000000000000000000, 0.000000000000000000, -0.000000000000000000 ) ) ;
#10779=PLANE ( 'NONE',  #11554 ) ;
#10784=ORIENTED_EDGE ( 'NONE', *, *, #5228, .F. ) ;
#10788=FACE_OUTER_BOUND ( 'NONE', #4537, .T. ) ;
#10807=CARTESIAN_POINT ( 'NONE',  ( 6.541334450618642826, 2.987059910623326875, 5.112749838330405083 ) ) ;
#10814=DIRECTION ( 'NONE',  ( 0.000000000000000000, 0.000000000000000000, -1.000000000000000000 ) ) ;
#10824=DIRECTION ( 'NONE',  ( -1.000000000000000000, -0.000000000000000000, -0.000000000000000000 ) ) ;
#10855=VERTEX_POINT ( 'NONE', #3437 ) ;
#10872=CARTESIAN_POINT ( 'NONE',  ( -2.915605589912154091E-15, 3.838309248099015747, 3.351853367131007566 ) ) ;
#10892=CARTESIAN_POINT ( 'NONE',  ( 6.207671477328661425, 5.338259717474330479, 0.7538629453361838095 ) ) ;
#10928=ADVANCED_FACE ( 'NONE', ( #6624 ), #8902, .F. ) ;
#10936=DIRECTION ( 'NONE',  ( 0.000000000000000000, 0.000000000000000000, 1.000000000000000000 ) ) ;
#10940=EDGE_LOOP ( 'NONE', ( #7824, #7219, #3974, #1772, #332 ) ) ;
#10945=CARTESIAN_POINT ( 'NONE',  ( 6.204449577088272605, 0.9975080636026212311, 5.000000000000000000 ) ) ;
#10971=ORIENTED_EDGE ( 'NONE', *, *, #8148, .T. ) ;
#10981=CARTESIAN_POINT ( 'NONE',  ( 6.367873360227558344, -2.886751345948133984, -5.000000000000000000 ) ) ;
#10983=ORIENTED_EDGE ( 'NONE', *, *, #10150, .T. ) ;
#10990=DIRECTION ( 'NONE',  ( 0.000000000000000000, 0.000000000000000000, 1.000000000000000000 ) ) ;
#11023=EDGE_LOOP ( 'NONE', ( #1305, #670, #12389, #13243 ) ) ;
#11032=CARTESIAN_POINT ( 'NONE',  ( 6.541333988313477121, -2.987057409892287740, -5.112749828287758369 ) ) ;
#11042=VERTEX_POINT ( 'NONE', #4747 ) ;
#11044=EDGE_CURVE ( 'NONE', #8372, #3318, #4384, .T. ) ;
#11047=PRODUCT ( 'hex flange bolt small_iso_ISO 4162 - M8 x 45 x 22-N', 'hex flange bolt small_iso_ISO 4162 - M8 x 45 x 22-N', '', ( #766 ) ) ;
#11086=DIRECTION ( 'NONE',  ( -1.000000000000000000, -0.000000000000000000, -0.000000000000000000 ) ) ;
#11100=CARTESIAN_POINT ( 'NONE',  ( 6.506891779418573662, 2.833891091414751706, 5.091556646552823473 ) ) ;
#11113=CARTESIAN_POINT ( 'NONE',  ( 6.244297270354684848, -1.798312406574552930E-11, -5.105276777067894400 ) ) ;
#11115=CARTESIAN_POINT ( 'NONE',  ( 6.196878017913834746, -5.292377467571577121, -0.8333333333333331483 ) ) ;
#11134=CARTESIAN_POINT ( 'NONE',  ( 0.1973348417602470706, -1.936114729415141733, 4.999999999999999112 ) ) ;
#11179=AXIS2_PLACEMENT_3D ( 'NONE', #9140, #3880, #7139 ) ;
#11183=ORIENTED_EDGE ( 'NONE', *, *, #11044, .F. ) ;
#11185=CARTESIAN_POINT ( 'NONE',  ( 6.527192678185835817, -2.941622124011024297, -5.095038975456044561 ) ) ;
#11251=VERTEX_POINT ( 'NONE', #9102 ) ;
#11258=DIRECTION ( 'NONE',  ( 1.000000000000000000, 0.000000000000000000, 0.000000000000000000 ) ) ;
#11262=CARTESIAN_POINT ( 'NONE',  ( 6.367873360227556567, 2.886751345948125991, 4.999999999999999112 ) ) ;
#11269=ORIENTED_EDGE ( 'NONE', *, *, #3924, .T. ) ;
#11276=EDGE_CURVE ( 'NONE', #5998, #8131, #6420, .T. ) ;
#11294=STYLED_ITEM('',(#13712),#5623);
#11297=CARTESIAN_POINT ( 'NONE',  ( 6.244297270354683960, 1.802013835206515036E-11, 5.105276777067893512 ) ) ;
#11312=CARTESIAN_POINT ( 'NONE',  ( 6.327625087026996553, 2.033113452595566972, -4.999999999998725464 ) ) ;
#11321=ORIENTED_EDGE ( 'NONE', *, *, #2783, .F. ) ;
#11326=CARTESIAN_POINT ( 'NONE',  ( 6.367873360227559232, -5.773502691896263528, 0.000000000000000000 ) ) ;
#11330=CLOSED_SHELL ( 'NONE', ( #4937, #1263, #1013, #3146, #4169, #10022, #395, #13385, #11524, #8255, #10148, #13261, #8879, #11463, #10725, #3150, #9314, #8986, #4390, #446, #10928, #3396, #7684, #8478, #7357, #7557, #9881, #6961, #12795 ) ) ;
#11335=B_SPLINE_CURVE_WITH_KNOTS ( 'NONE', 3,
 ( #4769, #8980, #8016, #2685, #11185, #8089, #12225, #12090, #656, #7947, #12295, #13387, #12160, #6025, #13180, #6910 ),
 .UNSPECIFIED., .F., .F.,
 ( 4, 3, 3, 3, 3, 4 ),
 ( -2.669610558406318528E-06, 0.000000000000000000, 5.703179328867203279E-05, 0.0001157653700806028548, 0.0001686517580799736817, 0.0002219032271235106112 ),
 .UNSPECIFIED. ) ;
#11340=VERTEX_POINT ( 'NONE', #5443 ) ;
#11355=VERTEX_POINT ( 'NONE', #8544 ) ;
#11362=CARTESIAN_POINT ( 'NONE',  ( 0.1983443223721567394, 3.359771601077105707, -4.180704885107416224 ) ) ;
#11395=ORIENTED_EDGE ( 'NONE', *, *, #3811, .F. ) ;
#11422=ORIENTED_EDGE ( 'NONE', *, *, #11521, .F. ) ;
#11441=EDGE_CURVE ( 'NONE', #12021, #9971, #4850, .T. ) ;
#11450=SURFACE_STYLE_FILL_AREA ( #12555 ) ;
#11463=ADVANCED_FACE ( 'NONE', ( #5637 ), #8156, .T. ) ;
#11464=ORIENTED_EDGE ( 'NONE', *, *, #1729, .T. ) ;
#11466=( GEOMETRIC_REPRESENTATION_CONTEXT ( 3 ) GLOBAL_UNCERTAINTY_ASSIGNED_CONTEXT ( ( #4675 ) ) GLOBAL_UNIT_ASSIGNED_CONTEXT ( ( #9384, #3087, #3019 ) ) REPRESENTATION_CONTEXT ( 'NONE', 'WORKASPACE' ) );
#11481=ORIENTED_EDGE ( 'NONE', *, *, #10570, .T. ) ;
#11502=AXIS2_PLACEMENT_3D ( 'NONE', #9693, #3404, #3813 ) ;
#11505=EDGE_CURVE ( 'NONE', #7289, #4363, #4914, .T. ) ;
#11521=EDGE_CURVE ( 'NONE', #11042, #13345, #4251, .T. ) ;
#11524=ADVANCED_FACE ( 'NONE', ( #13010 ), #10574, .T. ) ;
#11527=EDGE_CURVE ( 'NONE', #10855, #5998, #4590, .T. ) ;
#11541=DIRECTION ( 'NONE',  ( 1.000000000000000000, 0.000000000000000000, 0.000000000000000000 ) ) ;
#11554=AXIS2_PLACEMENT_3D ( 'NONE', #9551, #9618, #1298 ) ;
#11561=CARTESIAN_POINT ( 'NONE',  ( 6.092449800118089343, -3.827241605636891641, 3.371023086195408247 ) ) ;
#11572=CARTESIAN_POINT ( 'NONE',  ( 6.506987859255528583, 2.925375531177297095, -5.066899051217877314 ) ) ;
#11579=CARTESIAN_POINT ( 'NONE',  ( 6.534838248920896930, -2.951765777552406878, 5.112608298763836601 ) ) ;
#11622=CARTESIAN_POINT ( 'NONE',  ( 6.390820841722131718, -5.837016270311242039, -0.1100087447852515082 ) ) ;
#11629=EDGE_LOOP ( 'NONE', ( #12693, #13347, #10315, #2035 ) ) ;
#11633=CARTESIAN_POINT ( 'NONE',  ( 6.452281807715811723, 5.797857616945992554, -1.918911630784297550E-16 ) ) ;
#11672=CARTESIAN_POINT ( 'NONE',  ( 8.500000000000000000, 0.000000000000000000, 0.000000000000000000 ) ) ;
#11689=EDGE_LOOP ( 'NONE', ( #7006, #5546, #5239 ) ) ;
#11709=PLANE ( 'NONE',  #3638 ) ;
#11713=CARTESIAN_POINT ( 'NONE',  ( 6.481779955677433591, 2.910222513313285742, 5.040653254389411586 ) ) ;
#11723=DIRECTION ( 'NONE',  ( -1.000000000000000000, -0.000000000000000000, 0.000000000000000000 ) ) ;
#11726=EDGE_LOOP ( 'NONE', ( #6017, #5498 ) ) ;
#11733=( BOUNDED_SURFACE ( )  B_SPLINE_SURFACE ( 3, 2, ( 
 ( #10058, #11100, #8966 ),
 ( #7732, #11937, #2456 ),
 ( #12010, #2667, #6695 ),
 ( #1687, #6760, #5867 ),
 ( #10892, #1412, #5727 ),
 ( #9992, #5659, #8000 ) ),
 .UNSPECIFIED., .F., .F., .F. ) 
 B_SPLINE_SURFACE_WITH_KNOTS ( ( 4, 2, 4 ),
 ( 3, 3 ),
 ( 0.02367865728600889244, 0.02663179453327095547, 0.02958493178053301503 ),
 ( 0.000000000000000000, 1.000000000000000000 ),
 .UNSPECIFIED. ) 
 GEOMETRIC_REPRESENTATION_ITEM ( )  RATIONAL_B_SPLINE_SURFACE ( (
 ( 1.000000000000000000, 0.8047781103519378032, 1.000000000000000000),
 ( 1.000000000000000000, 0.8123785825977077879, 1.000000000000000000),
 ( 1.000000000000000000, 0.8190671539292031511, 1.000000000000000000),
 ( 1.000000000000000000, 0.8192352255331103450, 1.000000000000000000),
 ( 1.000000000000000000, 0.8126129676838903526, 1.000000000000000000),
 ( 1.000000000000000000, 0.8047712537969723412, 1.000000000000000000) ) ) 
 REPRESENTATION_ITEM ( '' )  SURFACE ( )  );
#11766=CARTESIAN_POINT ( 'NONE',  ( 53.50000000000000000, 0.000000000000000000, 3.309499999999999886 ) ) ;
#11774=CARTESIAN_POINT ( 'NONE',  ( 0.01055556052338981095, 4.575665857285978078, 2.074714256722482997 ) ) ;
#11791=CARTESIAN_POINT ( 'NONE',  ( 6.518095160331716542, -5.866179305615093931, 2.176274696337492837E-17 ) ) ;
#11794=EDGE_LOOP ( 'NONE', ( #1811, #2822 ) ) ;
#11812=ORIENTED_EDGE ( 'NONE', *, *, #2788, .F. ) ;
#11821=B_SPLINE_CURVE_WITH_KNOTS ( 'NONE', 3,
 ( #6267, #971, #10525, #9488, #5223, #11633, #13558, #4168, #5082, #4305, #4034, #9557, #1947, #9426, #5286, #12460 ),
 .UNSPECIFIED., .F., .F.,
 ( 4, 3, 3, 3, 3, 4 ),
 ( 0.000000000000000000, 5.303647860849293065E-05, 0.0001057093501027226378, 0.0001642058037231607288, 0.0002210073443958831293, 0.0002236769549542879461 ),
 .UNSPECIFIED. ) ;
#11838=CARTESIAN_POINT ( 'NONE',  ( 6.196878017913830305, 5.292377467571572680, -0.8333333333333333703 ) ) ;
#11847=CARTESIAN_POINT ( 'NONE',  ( 0.000000000000000000, -4.330127018922188320, 2.500000000000010214 ) ) ;
#11848=CARTESIAN_POINT ( 'NONE',  ( 6.245835795331710294, -1.036512332922514767, 5.105321605219339531 ) ) ;
#11849=EDGE_CURVE ( 'NONE', #5736, #10124, #7622, .T. ) ;
#11873=B_SPLINE_CURVE_WITH_KNOTS ( 'NONE', 3,
 ( #5231, #7370, #3274, #11579 ),
 .UNSPECIFIED., .F., .F.,
 ( 4, 4 ),
 ( 0.002977824986803813152, 0.005972417098209346735 ),
 .UNSPECIFIED. ) ;
#11874=DIRECTION ( 'NONE',  ( 0.000000000000000000, 0.000000000000000000, 1.000000000000000000 ) ) ;
#11889=CARTESIAN_POINT ( 'NONE',  ( 8.500000000000000000, 0.000000000000000000, 4.000000000000000000 ) ) ;
#11900=CARTESIAN_POINT ( 'NONE',  ( -4.878909776184767981E-16, 0.4887495715076933811, 4.999999999999999112 ) ) ;
#11937=CARTESIAN_POINT ( 'NONE',  ( 6.327632967268630004, 3.313549392874629795, 4.260764098153893897 ) ) ;
#11948=VERTEX_POINT ( 'NONE', #8574 ) ;
#11969=ORIENTED_EDGE ( 'NONE', *, *, #11521, .T. ) ;
#11977=VECTOR ( 'NONE', #7161, 1000.000000000000000 ) ;
#12010=CARTESIAN_POINT ( 'NONE',  ( 6.095473853218515536, 3.806361898857873793, 3.407187799183811983 ) ) ;
#12021=VERTEX_POINT ( 'NONE', #3254 ) ;
#12072=DIRECTION ( 'NONE',  ( -1.000000000000000000, 0.000000000000000000, -0.000000000000000000 ) ) ;
#12076=FACE_OUTER_BOUND ( 'NONE', #7825, .T. ) ;
#12079=CARTESIAN_POINT ( 'NONE',  ( 6.323268674613562013, -2.010012106699304191, -5.000000000001305622 ) ) ;
#12088=CARTESIAN_POINT ( 'NONE',  ( 6.271006797790669829, -0.9853839345309097775, -5.106080050406711202 ) ) ;
#12090=CARTESIAN_POINT ( 'NONE',  ( 6.495567275915079541, -2.917443832164891226, -5.053160945538031967 ) ) ;
#12099=EDGE_CURVE ( 'NONE', #8346, #7656, #5723, .T. ) ;
#12110=CARTESIAN_POINT ( 'NONE',  ( -4.997494388800372001E-16, -0.4883827417527024095, 4.999999999999999112 ) ) ;
#12122=DIRECTION ( 'NONE',  ( 0.000000000000000000, 0.000000000000000000, -1.000000000000000000 ) ) ;
#12134=PLANE ( 'NONE',  #4969 ) ;
#12137=PRODUCT_DEFINITION_CONTEXT ( 'detailed design', #6389, 'design' ) ;
#12144=DIRECTION ( 'NONE',  ( -1.000000000000000000, -0.000000000000000000, -0.000000000000000000 ) ) ;
#12160=CARTESIAN_POINT ( 'NONE',  ( 6.420058897733093239, -2.891482565094600776, -5.008194711943422917 ) ) ;
#12176=CARTESIAN_POINT ( 'NONE',  ( 8.500000000000000000, 4.898587196589412829E-16, -4.000000000000000000 ) ) ;
#12225=CARTESIAN_POINT ( 'NONE',  ( 6.506987859255520590, -2.925375531177299759, -5.066899051217866656 ) ) ;
#12239=CARTESIAN_POINT ( 'NONE',  ( 0.1739375980333479343, -3.358985280702903253, -4.182066831946573693 ) ) ;
#12286=APPLICATION_CONTEXT ( 'automotive_design' ) ;
#12295=CARTESIAN_POINT ( 'NONE',  ( 6.452281807715810835, -2.898928808472999830, -5.021091983800332947 ) ) ;
#12331=CARTESIAN_POINT ( 'NONE',  ( 6.445379721942638973, 2.463581311471617852, 5.110653333236676588 ) ) ;
#12334=CARTESIAN_POINT ( 'NONE',  ( 7.336184427528458230, 0.000000000000000000, 0.000000000000000000 ) ) ;
#12356=VERTEX_POINT ( 'NONE', #4980 ) ;
#12389=ORIENTED_EDGE ( 'NONE', *, *, #13529, .T. ) ;
#12404=ORIENTED_EDGE ( 'NONE', *, *, #3924, .F. ) ;
#12408=VERTEX_POINT ( 'NONE', #1143 ) ;
#12411=FACE_OUTER_BOUND ( 'NONE', #8877, .T. ) ;
#12412=CARTESIAN_POINT ( 'NONE',  ( 6.507056315241516842, -5.826803161468474102, 0.09231912136634916333 ) ) ;
#12425=DIRECTION ( 'NONE',  ( 0.000000000000000000, 0.000000000000000000, -1.000000000000000000 ) ) ;
#12438=ORIENTED_EDGE ( 'NONE', *, *, #1514, .F. ) ;
#12441=EDGE_CURVE ( 'NONE', #10124, #3640, #2397, .T. ) ;
#12456=ORIENTED_EDGE ( 'NONE', *, *, #5620, .F. ) ;
#12460=CARTESIAN_POINT ( 'NONE',  ( 6.534838248920899595, 5.903531555104835071, 8.098083288904839678E-18 ) ) ;
#12461=CARTESIAN_POINT ( 'NONE',  ( 0.01055556052338940676, 4.084588180558400339, -2.925285743277528105 ) ) ;
#12484=CARTESIAN_POINT ( 'NONE',  ( 6.092449800118536096, -4.833012432206597708, -1.628976913806147397 ) ) ;
#12502=CARTESIAN_POINT ( 'NONE',  ( 6.445127866599364097, -3.194847394660946360, 4.687657648742338701 ) ) ;
#12508=B_SPLINE_CURVE_WITH_KNOTS ( 'NONE', 3,
 ( #9613, #9348, #12585, #4019, #10579, #2071, #3116, #1085 ),
 .UNSPECIFIED., .F., .F.,
 ( 4, 2, 2, 4 ),
 ( 1.228285202167177233E-19, 0.001493104274552340370, 0.002986208549104680306, 0.005972417098209360613 ),
 .UNSPECIFIED. ) ;
#12526=EDGE_LOOP ( 'NONE', ( #3057, #8010, #5547, #595 ) ) ;
#12533=CARTESIAN_POINT ( 'NONE',  ( 0.000000000000000000, 4.330127018922190096, -2.500000000000006217 ) ) ;
#12546=DIRECTION ( 'NONE',  ( 1.000000000000000000, 0.000000000000000000, -0.000000000000000000 ) ) ;
#12551=CARTESIAN_POINT ( 'NONE',  ( 6.534224484704324709, 2.950930484791589148, 5.111161529262913561 ) ) ;
#12553=CARTESIAN_POINT ( 'NONE',  ( 6.327632967270859332, 5.346704644972003706, -0.7392359018481428068 ) ) ;
#12555=FILL_AREA_STYLE ('',( #6079 ) ) ;
#12585=CARTESIAN_POINT ( 'NONE',  ( 6.371506350351447523, -5.409331239960139648, -0.8483282427581471108 ) ) ;
#12637=CARTESIAN_POINT ( 'NONE',  ( 8.500000000000000000, 0.000000000000000000, 0.000000000000000000 ) ) ;
#12638=FACE_OUTER_BOUND ( 'NONE', #10940, .T. ) ;
#12693=ORIENTED_EDGE ( 'NONE', *, *, #5704, .T. ) ;
#12712=AXIS2_PLACEMENT_3D ( 'NONE', #2101, #1049, #3149 ) ;
#12726=CARTESIAN_POINT ( 'NONE',  ( 6.403457969954085449, 2.888443235695447253, -5.002930439003170804 ) ) ;
#12736=DIRECTION ( 'NONE',  ( -0.000000000000000000, 0.8660254037844387076, 0.5000000000000001110 ) ) ;
#12749=CARTESIAN_POINT ( 'NONE',  ( 6.481779955677436256, -5.820445026626584806, 1.740800559574606662E-15 ) ) ;
#12774=VECTOR ( 'NONE', #7642, 1000.000000000000000 ) ;
#12795=ADVANCED_FACE ( 'NONE', ( #12411 ), #6309, .F. ) ;
#12813=DIRECTION ( 'NONE',  ( 0.000000000000000000, 0.000000000000000000, 1.000000000000000000 ) ) ;
#12842=AXIS2_PLACEMENT_3D ( 'NONE', #6948, #6064, #3762 ) ;
#12856=EDGE_LOOP ( 'NONE', ( #10039, #11269, #8975 ) ) ;
#12873=CARTESIAN_POINT ( 'NONE',  ( 6.367873360227555679, -2.886751345948119774, 4.999999999999999112 ) ) ;
#12889=CIRCLE ( 'NONE', #2749, 7.900000000000002132 ) ;
#12907=ORIENTED_EDGE ( 'NONE', *, *, #5080, .F. ) ;
#12910=CARTESIAN_POINT ( 'NONE',  ( 0.000000000000000000, 0.000000000000000000, 0.000000000000000000 ) ) ;
#12913=CARTESIAN_POINT ( 'NONE',  ( 6.534838248920896930, -2.951765777552406878, 5.112608298763836601 ) ) ;
#12932=EDGE_CURVE ( 'NONE', #1735, #10124, #2061, .T. ) ;
#12933=DIRECTION ( 'NONE',  ( 0.3420201433256622736, 1.150791560227853228E-16, 0.9396926207859106484 ) ) ;
#12940=CARTESIAN_POINT ( 'NONE',  ( 0.4465819873852002742, 2.886751345948125547, 4.999999999999999112 ) ) ;
#12952=EDGE_LOOP ( 'NONE', ( #798, #3671, #10053 ) ) ;
#12975=DIRECTION ( 'NONE',  ( 1.000000000000000000, 0.000000000000000000, -0.000000000000000000 ) ) ;
#12986=B_SPLINE_CURVE_WITH_KNOTS ( 'NONE', 3,
 ( #1112, #6535, #11774, #7566, #90, #2359, #1244, #9770 ),
 .UNSPECIFIED., .F., .F.,
 ( 4, 2, 2, 4 ),
 ( 0.002921158011986707288, 0.003648658599403064012, 0.004376159186819420302, 0.005831160361652131148 ),
 .UNSPECIFIED. ) ;
#12996=MECHANICAL_DESIGN_GEOMETRIC_PRESENTATION_REPRESENTATION('',(#9269),#11466);
#13002=DIRECTION ( 'NONE',  ( 1.000000000000000000, 0.000000000000000000, 0.000000000000000000 ) ) ;
#13010=FACE_OUTER_BOUND ( 'NONE', #13144, .T. ) ;
#13020=CARTESIAN_POINT ( 'NONE',  ( 6.534838248920899595, 5.903531555104835071, 8.098083288904839678E-18 ) ) ;
#13028=EDGE_CURVE ( 'NONE', #4029, #5480, #83, .T. ) ;
#13077=CARTESIAN_POINT ( 'NONE',  ( 6.367873360227558344, -2.886751345948133984, -5.000000000000000000 ) ) ;
#13081=CARTESIAN_POINT ( 'NONE',  ( 6.092439126518621073, 1.005559546149547678, 4.999999999999999112 ) ) ;
#13104=CARTESIAN_POINT ( 'NONE',  ( 6.204471256525345702, -0.9979289516723606202, -5.000000000000889955 ) ) ;
#13144=EDGE_LOOP ( 'NONE', ( #10784, #2620, #7620, #507, #8710, #4746, #10230 ) ) ;
#13148=CIRCLE ( 'NONE', #7217, 0.5999999999999980904 ) ;
#13167=CARTESIAN_POINT ( 'NONE',  ( 6.362366615495708366, 2.018765416950190961, -5.108861542006171597 ) ) ;
#13176=ORIENTED_EDGE ( 'NONE', *, *, #6787, .F. ) ;
#13180=CARTESIAN_POINT ( 'NONE',  ( 6.385552186430389021, -2.886751345948133984, -5.000000000000000000 ) ) ;
#13187=ORIENTED_EDGE ( 'NONE', *, *, #11527, .F. ) ;
#13231=DIRECTION ( 'NONE',  ( 1.000000000000000000, 0.000000000000000000, -0.000000000000000000 ) ) ;
#13243=ORIENTED_EDGE ( 'NONE', *, *, #6291, .F. ) ;
#13250=CARTESIAN_POINT ( 'NONE',  ( 6.367873360227558344, 5.773502691896261751, 0.000000000000000000 ) ) ;
#13261=ADVANCED_FACE ( 'NONE', ( #8883 ), #4737, .T. ) ;
#13262=CARTESIAN_POINT ( 'NONE',  ( 6.196878017913830305, -1.924500897298744961, 4.999999999999999112 ) ) ;
#13265=CARTESIAN_POINT ( 'NONE',  ( 6.534838248920899595, -2.951765777552420644, -5.112608298763837489 ) ) ;
#13271=CARTESIAN_POINT ( 'NONE',  ( 0.000000000000000000, 4.330127018922190096, -2.500000000000006217 ) ) ;
#13281=EDGE_CURVE ( 'NONE', #9971, #5480, #3387, .T. ) ;
#13283=AXIS2_PLACEMENT_3D ( 'NONE', #9276, #10093, #602 ) ;
#13284=CARTESIAN_POINT ( 'NONE',  ( 53.50000000000000000, 0.000000000000000000, 0.000000000000000000 ) ) ;
#13290=DIRECTION ( 'NONE',  ( -1.000000000000000000, -0.000000000000000000, -0.000000000000000000 ) ) ;
#13299=CARTESIAN_POINT ( 'NONE',  ( 6.436591462021362453, -2.894509378375957009, 5.013437306331779197 ) ) ;
#13345=VERTEX_POINT ( 'NONE', #693 ) ;
#13347=ORIENTED_EDGE ( 'NONE', *, *, #8802, .F. ) ;
#13349=EDGE_CURVE ( 'NONE', #5480, #6095, #3872, .T. ) ;
#13358=CARTESIAN_POINT ( 'NONE',  ( 6.244297270355323448, 0.4917101305082447471, 5.105276777067912164 ) ) ;
#13368=CARTESIAN_POINT ( 'NONE',  ( 6.541171661047877173, -2.934678558896545386, -5.142480235691130552 ) ) ;
#13372=CARTESIAN_POINT ( 'NONE',  ( 0.3108895250736384841, -2.416698868092693075, -5.000000000000000000 ) ) ;
#13385=ADVANCED_FACE ( 'NONE', ( #9292 ), #3828, .F. ) ;
#13386=DIRECTION ( 'NONE',  ( 0.000000000000000000, 0.000000000000000000, 1.000000000000000000 ) ) ;
#13387=CARTESIAN_POINT ( 'NONE',  ( 6.436591462021357124, -2.894509378375969000, -5.013437306331776533 ) ) ;
#13482=ORIENTED_EDGE ( 'NONE', *, *, #8638, .F. ) ;
#13487=DIRECTION ( 'NONE',  ( 0.000000000000000000, -0.8660254037844380415, 0.5000000000000011102 ) ) ;
#13502=ORIENTED_EDGE ( 'NONE', *, *, #5228, .T. ) ;
#13505=CARTESIAN_POINT ( 'NONE',  ( 6.541334219041337050, 2.934241909852039143, -5.143243597038033244 ) ) ;
#13506=CARTESIAN_POINT ( 'NONE',  ( 6.452281807715817941, -2.898928808472988283, 5.021091983800338276 ) ) ;
#13529=EDGE_CURVE ( 'NONE', #9438, #11340, #6462, .T. ) ;
#13543=CARTESIAN_POINT ( 'NONE',  ( 6.390983399715589819, -2.822795037344614233, 5.110775575965824657 ) ) ;
#13558=CARTESIAN_POINT ( 'NONE',  ( 6.466260427357665819, 5.808561367196023895, -1.902591328531564046E-16 ) ) ;
#13560=DIRECTION ( 'NONE',  ( -0.000000000000000000, 0.000000000000000000, 1.000000000000000000 ) ) ;
#13573=CARTESIAN_POINT ( 'NONE',  ( 0.000000000000000000, 4.330127018922190985, 2.500000000000005329 ) ) ;
#13577=ORIENTED_EDGE ( 'NONE', *, *, #11527, .T. ) ;
#13579=CARTESIAN_POINT ( 'NONE',  ( 6.390820841722129941, 5.837016270311235822, 0.1100087447852453187 ) ) ;
#13580=CARTESIAN_POINT ( 'NONE',  ( 6.390820551024316565, -3.013776919160863876, 4.999999999999999112 ) ) ;
#13600=CARTESIAN_POINT ( 'NONE',  ( 6.355827204229362870, -5.411702751981846582, 0.8440485055075620524 ) ) ;
#13613=DIRECTION ( 'NONE',  ( 0.000000000000000000, 0.000000000000000000, -1.000000000000000000 ) ) ;
#13642=DIRECTION ( 'NONE',  ( 1.000000000000000000, 0.000000000000000000, -0.000000000000000000 ) ) ;
#13649=B_SPLINE_CURVE_WITH_KNOTS ( 'NONE', 3,
 ( #3472, #11900, #5761, #5552, #9832, #285 ),
 .UNSPECIFIED., .F., .F.,
 ( 4, 2, 4 ),
 ( 0.008261945092156346496, 0.009724140865920691962, 0.01118633663968503569 ),
 .UNSPECIFIED. ) ;
#13706=COLOUR_RGB('Black',0.12,0.14,0.17);
#13707=FILL_AREA_STYLE_COLOUR('',#13706);
#13708=FILL_AREA_STYLE('',(#13707));
#13709=SURFACE_STYLE_FILL_AREA(#13708);
#13710=SURFACE_SIDE_STYLE('',(#13709));
#13711=SURFACE_STYLE_USAGE(.BOTH.,#13710);
#13712=PRESENTATION_STYLE_ASSIGNMENT((#13711));
ENDSEC;
END-ISO-10303-21;
